ISO-10303-21;
HEADER;
FILE_DESCRIPTION (('STEP AP214'),
    '1' );
FILE_NAME ('jaw_ISO - Spur gear 1M 15T 20PA 8FW ---S15A75H50L4.0N.step',
    '2026-10-03T18:28:46',
    ( '' ),
    ( '' ),
    'SwSTEP 2.0',
    'SolidWorks 2026',
    '' );
FILE_SCHEMA (( 'AUTOMOTIVE_DESIGN' ));
ENDSEC;

DATA;
#8=DIRECTION ( 'NONE',  ( 1.000000000000000000, -0.000000000000000000, -0.000000000000000000 ) ) ;
#11=AXIS2_PLACEMENT_3D ( 'NONE', #9784, #8139, #4791 ) ;
#17=CIRCLE ( 'NONE', #8645, 6.248999999999999666 ) ;
#23=EDGE_CURVE ( 'NONE', #8074, #935, #6750, .T. ) ;
#24=LINE ( 'NONE', #5186, #1032 ) ;
#25=VECTOR ( 'NONE', #10165, 1000.000000000000000 ) ;
#27=AXIS2_PLACEMENT_3D ( 'NONE', #3264, #1729, #5737 ) ;
#28=CARTESIAN_POINT ( 'NONE',  ( 8.000000000000001776, 7.008469740302810891, -0.7425307242147085596 ) ) ;
#34=AXIS2_PLACEMENT_3D ( 'NONE', #10379, #6382, #8043 ) ;
#35=ORIENTED_EDGE ( 'NONE', *, *, #573, .T. ) ;
#42=ORIENTED_EDGE ( 'NONE', *, *, #3976, .T. ) ;
#50=CARTESIAN_POINT ( 'NONE',  ( -2.000000000000000000, 4.137773741518453008, -5.705158055754754542 ) ) ;
#58=CARTESIAN_POINT ( 'NONE',  ( 10.00000000000000000, 5.904264776415100613, 2.046865518294722630 ) ) ;
#60=DIRECTION ( 'NONE',  ( 0.000000000000000000, 1.000000000000000000, -7.228014483236699822E-18 ) ) ;
#61=CIRCLE ( 'NONE', #8365, 3.000000000000000000 ) ;
#70=CIRCLE ( 'NONE', #566, 8.500000000000000000 ) ;
#71=CARTESIAN_POINT ( 'NONE',  ( 8.000000000000001776, -5.349675154362301122, -3.229702268444983648 ) ) ;
#73=CARTESIAN_POINT ( 'NONE',  ( 8.000000000000001776, -2.861184399890952079, -6.440778198864142823 ) ) ;
#85=MECHANICAL_DESIGN_GEOMETRIC_PRESENTATION_REPRESENTATION('',(#9215),#5323);
#88=CARTESIAN_POINT ( 'NONE',  ( 0.000000000000000000, 52.93638525830372998, 8.843061888689529582 ) ) ;
#90=AXIS2_PLACEMENT_3D ( 'NONE', #8331, #4928, #5764 ) ;
#101=ORIENTED_EDGE ( 'NONE', *, *, #1637, .T. ) ;
#111=CIRCLE ( 'NONE', #4663, 3.000000000000000000 ) ;
#112=LINE ( 'NONE', #6402, #5089 ) ;
#129=ADVANCED_FACE ( 'NONE', ( #8084 ), #5628, .T. ) ;
#133=ORIENTED_EDGE ( 'NONE', *, *, #9091, .T. ) ;
#141=EDGE_LOOP ( 'NONE', ( #4012, #8680, #9261, #9381 ) ) ;
#145=VERTEX_POINT ( 'NONE', #7277 ) ;
#153=EDGE_LOOP ( 'NONE', ( #2602, #8122, #9695, #3573 ) ) ;
#158=DIRECTION ( 'NONE',  ( -1.000000000000000000, -0.000000000000000000, -0.000000000000000000 ) ) ;
#166=MECHANICAL_DESIGN_GEOMETRIC_PRESENTATION_REPRESENTATION('',(#664),#9477);
#168=CIRCLE ( 'NONE', #6585, 2.999999999999999112 ) ;
#174=CARTESIAN_POINT ( 'NONE',  ( 8.000000000000001776, 5.241389472434725860, -4.711457988287000909 ) ) ;
#177=CARTESIAN_POINT ( 'NONE',  ( 10.00000000000000000, -5.233522515400119701, 4.720195129223260899 ) ) ;
#185=AXIS2_PLACEMENT_3D ( 'NONE', #7791, #8589, #2122 ) ;
#188=AXIS2_PLACEMENT_3D ( 'NONE', #2496, #158, #4930 ) ;
#190=CIRCLE ( 'NONE', #4074, 3.000000000000000000 ) ;
#195=CIRCLE ( 'NONE', #5093, 3.000000000000000000 ) ;
#196=CARTESIAN_POINT ( 'NONE',  ( 8.000000000000001776, -4.724769925181144359, -4.089810527897808079 ) ) ;
#201=VERTEX_POINT ( 'NONE', #9239 ) ;
#213=EDGE_CURVE ( 'NONE', #3364, #1830, #6075, .T. ) ;
#214=FILL_AREA_STYLE_COLOUR ( '', #3785 ) ;
#216=VERTEX_POINT ( 'NONE', #1872 ) ;
#218=CARTESIAN_POINT ( 'NONE',  ( 4.000000000000000888, 8.357095590591340439, -1.552080310331536372 ) ) ;
#219=DIRECTION ( 'NONE',  ( -1.000000000000000000, -0.000000000000000000, -0.000000000000000000 ) ) ;
#227=EDGE_CURVE ( 'NONE', #7607, #7874, #10094, .T. ) ;
#234=DIRECTION ( 'NONE',  ( -1.000000000000000000, -0.000000000000000000, -0.000000000000000000 ) ) ;
#238=AXIS2_PLACEMENT_3D ( 'NONE', #8296, #9037, #6583 ) ;
#240=ORIENTED_EDGE ( 'NONE', *, *, #4869, .F. ) ;
#250=ORIENTED_EDGE ( 'NONE', *, *, #7768, .T. ) ;
#253=EDGE_CURVE ( 'NONE', #3846, #7785, #9133, .T. ) ;
#254=CARTESIAN_POINT ( 'NONE',  ( 8.000000000000001776, 0.000000000000000000, 0.000000000000000000 ) ) ;
#280=AXIS2_PLACEMENT_3D ( 'NONE', #7224, #4941, #9679 ) ;
#282=VECTOR ( 'NONE', #6359, 1000.000000000000000 ) ;
#285=DIRECTION ( 'NONE',  ( 0.000000000000000000, 0.000000000000000000, 1.000000000000000000 ) ) ;
#288=ADVANCED_FACE ( 'NONE', ( #384 ), #8291, .T. ) ;
#296=ORIENTED_EDGE ( 'NONE', *, *, #1709, .F. ) ;
#304=ORIENTED_EDGE ( 'NONE', *, *, #4469, .T. ) ;
#305=CARTESIAN_POINT ( 'NONE',  ( -2.000000000000000000, -2.861184399890952079, -6.440778198864142823 ) ) ;
#328=EDGE_CURVE ( 'NONE', #7607, #1777, #2963, .T. ) ;
#330=DIRECTION ( 'NONE',  ( -1.000000000000000000, -0.000000000000000000, -0.000000000000000000 ) ) ;
#337=AXIS2_PLACEMENT_3D ( 'NONE', #4333, #7524, #4129 ) ;
#344=CYLINDRICAL_SURFACE ( 'NONE', #7027, 8.500000000000000000 ) ;
#346=VERTEX_POINT ( 'NONE', #10198 ) ;
#347=AXIS2_PLACEMENT_3D ( 'NONE', #3685, #9425, #2154 ) ;
#352=ORIENTED_EDGE ( 'NONE', *, *, #7205, .T. ) ;
#371=VERTEX_POINT ( 'NONE', #1326 ) ;
#380=DIRECTION ( 'NONE',  ( 0.000000000000000000, 0.000000000000000000, 1.000000000000000000 ) ) ;
#382=EDGE_CURVE ( 'NONE', #3846, #7164, #6301, .T. ) ;
#384=FACE_OUTER_BOUND ( 'NONE', #2361, .T. ) ;
#392=FACE_OUTER_BOUND ( 'NONE', #3063, .T. ) ;
#395=ORIENTED_EDGE ( 'NONE', *, *, #7205, .F. ) ;
#402=ORIENTED_EDGE ( 'NONE', *, *, #10343, .F. ) ;
#408=CARTESIAN_POINT ( 'NONE',  ( 10.00000000000000000, 6.100541242131515496, -3.528937025535514138 ) ) ;
#413=ORIENTED_EDGE ( 'NONE', *, *, #3949, .T. ) ;
#422=DIRECTION ( 'NONE',  ( 0.000000000000000000, -2.602085213965211430E-15, -1.000000000000000000 ) ) ;
#423=DIRECTION ( 'NONE',  ( 0.000000000000000000, 0.000000000000000000, 1.000000000000000000 ) ) ;
#427=EDGE_CURVE ( 'NONE', #9096, #1645, #4210, .T. ) ;
#429=DIRECTION ( 'NONE',  ( 0.000000000000000000, 0.000000000000000000, 1.000000000000000000 ) ) ;
#430=CARTESIAN_POINT ( 'NONE',  ( 8.000000000000001776, 6.100541242131515496, 3.528937025535514138 ) ) ;
#435=DIRECTION ( 'NONE',  ( 0.000000000000000000, 0.000000000000000000, 1.000000000000000000 ) ) ;
#455=DIRECTION ( 'NONE',  ( 1.000000000000000000, 0.000000000000000000, 0.000000000000000000 ) ) ;
#458=CARTESIAN_POINT ( 'NONE',  ( -2.000000000000000000, 4.438567988583180579, -7.249076783337634389 ) ) ;
#464=CARTESIAN_POINT ( 'NONE',  ( -2.000000000000000000, 6.704570150427012543, -2.172265885002586661 ) ) ;
#467=VERTEX_POINT ( 'NONE', #7099 ) ;
#470=EDGE_CURVE ( 'NONE', #6865, #935, #9468, .T. ) ;
#477=CARTESIAN_POINT ( 'NONE',  ( 0.000000000000000000, 52.93638525830372998, 2.343061888689529582 ) ) ;
#482=CARTESIAN_POINT ( 'NONE',  ( 8.000000000000001776, -5.979767908488829775, -1.814490771706245065 ) ) ;
#483=LINE ( 'NONE', #7749, #4325 ) ;
#484=LINE ( 'NONE', #6725, #1123 ) ;
#501=ORIENTED_EDGE ( 'NONE', *, *, #2913, .F. ) ;
#508=ORIENTED_EDGE ( 'NONE', *, *, #573, .F. ) ;
#511=ADVANCED_FACE ( 'NONE', ( #10357 ), #2867, .T. ) ;
#529=EDGE_CURVE ( 'NONE', #5739, #8939, #8617, .T. ) ;
#537=DIRECTION ( 'NONE',  ( 0.000000000000000000, 0.000000000000000000, -1.000000000000000000 ) ) ;
#559=CARTESIAN_POINT ( 'NONE',  ( 50.00005079999999680, 0.000000000000000000, 2.000000000000000000 ) ) ;
#563=ORIENTED_EDGE ( 'NONE', *, *, #23, .F. ) ;
#566=AXIS2_PLACEMENT_3D ( 'NONE', #5875, #9125, #9777 ) ;
#569=FACE_OUTER_BOUND ( 'NONE', #4760, .T. ) ;
#571=ORIENTED_EDGE ( 'NONE', *, *, #4996, .F. ) ;
#573=EDGE_CURVE ( 'NONE', #4283, #2644, #1679, .T. ) ;
#580=PLANE ( 'NONE',  #2780 ) ;
#582=DIRECTION ( 'NONE',  ( 1.000000000000000000, 0.000000000000000000, 0.000000000000000000 ) ) ;
#591=CARTESIAN_POINT ( 'NONE',  ( 10.00000000000000000, 6.745408891279613961, -5.171987904998036178 ) ) ;
#598=EDGE_CURVE ( 'NONE', #2046, #5731, #3289, .T. ) ;
#601=CIRCLE ( 'NONE', #6521, 3.000000000000000000 ) ;
#607=EDGE_LOOP ( 'NONE', ( #3342, #10479, #6748, #9581 ) ) ;
#610=EDGE_CURVE ( 'NONE', #9996, #6690, #3028, .T. ) ;
#611=CIRCLE ( 'NONE', #6015, 6.248999999999999666 ) ;
#612=DIRECTION ( 'NONE',  ( 1.000000000000000000, 0.000000000000000000, 0.000000000000000000 ) ) ;
#626=CARTESIAN_POINT ( 'NONE',  ( -2.000000000000000000, 5.904264776415129923, -2.046865518294644914 ) ) ;
#630=ORIENTED_EDGE ( 'NONE', *, *, #598, .F. ) ;
#631=DIRECTION ( 'NONE',  ( 1.000000000000000000, 0.000000000000000000, -0.000000000000000000 ) ) ;
#632=DIRECTION ( 'NONE',  ( 0.000000000000000000, 0.000000000000000000, 1.000000000000000000 ) ) ;
#645=CARTESIAN_POINT ( 'NONE',  ( 8.000000000000001776, 4.561279057474473930, -4.271385531633122845 ) ) ;
#646=CARTESIAN_POINT ( 'NONE',  ( -2.000000000000000000, 7.008469740302810891, -0.7425307242147085596 ) ) ;
#651=PRESENTATION_STYLE_ASSIGNMENT (( #2303 ) ) ;
#652=DIRECTION ( 'NONE',  ( 0.000000000000000000, -1.154631945610162802E-14, -1.000000000000000000 ) ) ;
#657=AXIS2_PLACEMENT_3D ( 'NONE', #1217, #8778, #8485 ) ;
#661=DIRECTION ( 'NONE',  ( 0.000000000000000000, 0.000000000000000000, 1.000000000000000000 ) ) ;
#664=STYLED_ITEM ( 'NONE', ( #651 ), #1029 ) ;
#669=DIRECTION ( 'NONE',  ( 0.000000000000000000, 0.000000000000000000, 1.000000000000000000 ) ) ;
#671=EDGE_CURVE ( 'NONE', #6869, #4944, #2339, .T. ) ;
#672=AXIS2_PLACEMENT_3D ( 'NONE', #9186, #234, #7433 ) ;
#673=ORIENTED_EDGE ( 'NONE', *, *, #10174, .F. ) ;
#677=VECTOR ( 'NONE', #10171, 1000.000000000000000 ) ;
#683=ORIENTED_EDGE ( 'NONE', *, *, #7002, .F. ) ;
#686=CIRCLE ( 'NONE', #2043, 3.000000000000000888 ) ;
#689=ADVANCED_BREP_SHAPE_REPRESENTATION ( '', ( #1029, #2101 ), #5648 ) ;
#691=AXIS2_PLACEMENT_3D ( 'NONE', #2203, #3948, #9582 ) ;
#693=AXIS2_PLACEMENT_3D ( 'NONE', #10001, #3572, #9409 ) ;
#695=CARTESIAN_POINT ( 'NONE',  ( -2.000000000000000000, -2.652816298622379776, -5.657964889053610946 ) ) ;
#709=CARTESIAN_POINT ( 'NONE',  ( 4.000000000000000888, 8.265874651078044977, -1.981241088980697729 ) ) ;
#710=LINE ( 'NONE', #7975, #863 ) ;
#718=ORIENTED_EDGE ( 'NONE', *, *, #4535, .F. ) ;
#720=ORIENTED_EDGE ( 'NONE', *, *, #4047, .T. ) ;
#723=LINE ( 'NONE', #6220, #677 ) ;
#727=ORIENTED_EDGE ( 'NONE', *, *, #1997, .F. ) ;
#732=DIRECTION ( 'NONE',  ( 0.000000000000000000, 0.000000000000000000, -1.000000000000000000 ) ) ;
#733=ORIENTED_EDGE ( 'NONE', *, *, #2748, .F. ) ;
#737=DIRECTION ( 'NONE',  ( -1.000000000000000000, -0.000000000000000000, -0.000000000000000000 ) ) ;
#739=ORIENTED_EDGE ( 'NONE', *, *, #9069, .T. ) ;
#757=ORIENTED_EDGE ( 'NONE', *, *, #23, .T. ) ;
#765=CYLINDRICAL_SURFACE ( 'NONE', #10346, 8.500000000000000000 ) ;
#773=CARTESIAN_POINT ( 'NONE',  ( -2.000000000000000000, 2.871924938129970517, -6.435996203144478400 ) ) ;
#795=ADVANCED_FACE ( 'NONE', ( #7932 ), #3599, .T. ) ;
#801=LINE ( 'NONE', #3182, #7893 ) ;
#802=CARTESIAN_POINT ( 'NONE',  ( 4.000000000000000888, -5.522688772756355391, -6.461416928141300531 ) ) ;
#803=DIRECTION ( 'NONE',  ( 0.000000000000000000, 0.000000000000000000, 1.000000000000000000 ) ) ;
#826=CARTESIAN_POINT ( 'NONE',  ( -2.000000000000000000, 4.058600654062950674, -7.468451026206158083 ) ) ;
#836=CARTESIAN_POINT ( 'NONE',  ( -2.000000000000000000, 52.93638525830372998, 2.343061888689529582 ) ) ;
#837=VERTEX_POINT ( 'NONE', #2366 ) ;
#838=AXIS2_PLACEMENT_3D ( 'NONE', #8631, #1368, #3801 ) ;
#843=CLOSED_SHELL ( 'NONE', ( #7151, #129, #1567, #8897, #9633, #4992, #3175, #8197, #2905, #8321, #2086, #3112, #8363, #5266, #10473, #8475, #5747, #9474, #6974, #1129, #4223, #6918, #511, #2544, #4107, #7035, #6532, #8445, #5830, #8827, #288, #5462, #6321, #1838, #7810, #4341, #5967, #9961, #9615, #5841, #3362, #795, #9948, #6931, #5514, #4220, #8577, #2099, #3356, #8417 ) ) ;
#848=ORIENTED_EDGE ( 'NONE', *, *, #9343, .F. ) ;
#863=VECTOR ( 'NONE', #8661, 1000.000000000000000 ) ;
#869=CARTESIAN_POINT ( 'NONE',  ( -2.000000000000000000, 6.100541242131515496, 3.528937025535514138 ) ) ;
#882=DIRECTION ( 'NONE',  ( 0.000000000000000000, 0.000000000000000000, -1.000000000000000000 ) ) ;
#883=CARTESIAN_POINT ( 'NONE',  ( -10.00000000000000000, 0.000000000000000000, 0.000000000000000000 ) ) ;
#890=ORIENTED_EDGE ( 'NONE', *, *, #1809, .T. ) ;
#891=ORIENTED_EDGE ( 'NONE', *, *, #10393, .F. ) ;
#897=VERTEX_POINT ( 'NONE', #10082 ) ;
#903=DIRECTION ( 'NONE',  ( 1.000000000000000000, 0.000000000000000000, 0.000000000000000000 ) ) ;
#905=DIRECTION ( 'NONE',  ( -1.000000000000000000, -0.000000000000000000, 0.000000000000000000 ) ) ;
#913=CIRCLE ( 'NONE', #10073, 6.248999999999999666 ) ;
#915=CARTESIAN_POINT ( 'NONE',  ( -2.000000000000000000, 8.357095590591340439, 1.552080310331536372 ) ) ;
#926=EDGE_CURVE ( 'NONE', #6166, #7456, #7265, .T. ) ;
#935=VERTEX_POINT ( 'NONE', #8255 ) ;
#942=VECTOR ( 'NONE', #5802, 1000.000000000000000 ) ;
#943=ORIENTED_EDGE ( 'NONE', *, *, #1613, .F. ) ;
#950=ORIENTED_EDGE ( 'NONE', *, *, #5479, .T. ) ;
#951=AXIS2_PLACEMENT_3D ( 'NONE', #8240, #9127, #4244 ) ;
#962=ORIENTED_EDGE ( 'NONE', *, *, #10068, .T. ) ;
#963=CARTESIAN_POINT ( 'NONE',  ( 8.000000000000001776, 7.008469740302810891, -0.7425307242147085596 ) ) ;
#972=DIRECTION ( 'NONE',  ( 0.000000000000000000, 0.000000000000000000, 1.000000000000000000 ) ) ;
#978=DIRECTION ( 'NONE',  ( -1.000000000000000000, -0.000000000000000000, -0.000000000000000000 ) ) ;
#981=CARTESIAN_POINT ( 'NONE',  ( -2.000000000000000000, 0.000000000000000000, 0.000000000000000000 ) ) ;
#983=ORIENTED_EDGE ( 'NONE', *, *, #3850, .F. ) ;
#991=ORIENTED_EDGE ( 'NONE', *, *, #529, .F. ) ;
#1001=DIRECTION ( 'NONE',  ( 0.000000000000000000, 0.000000000000000000, 1.000000000000000000 ) ) ;
#1005=CARTESIAN_POINT ( 'NONE',  ( -2.000000000000000000, 6.391777940760639877E-17, 8.843061888689529582 ) ) ;
#1010=AXIS2_PLACEMENT_3D ( 'NONE', #6074, #2853, #1109 ) ;
#1015=LINE ( 'NONE', #3457, #6693 ) ;
#1018=CARTESIAN_POINT ( 'NONE',  ( 8.000000000000001776, 1.459547570502460978, -6.894905428400257996 ) ) ;
#1024=CIRCLE ( 'NONE', #9841, 2.000000000000000000 ) ;
#1025=DIRECTION ( 'NONE',  ( -1.000000000000000000, -0.000000000000000000, -0.000000000000000000 ) ) ;
#1029=MANIFOLD_SOLID_BREP ( 'Move Face1', #843 ) ;
#1031=CYLINDRICAL_SURFACE ( 'NONE', #2899, 8.500000000000000000 ) ;
#1032=VECTOR ( 'NONE', #3301, 1000.000000000000000 ) ;
#1047=EDGE_CURVE ( 'NONE', #8424, #3846, #3537, .T. ) ;
#1049=ORIENTED_EDGE ( 'NONE', *, *, #4497, .T. ) ;
#1053=ORIENTED_EDGE ( 'NONE', *, *, #3828, .T. ) ;
#1055=PRESENTATION_STYLE_ASSIGNMENT (( #6067 ) ) ;
#1056=EDGE_LOOP ( 'NONE', ( #5495, #10274, #1904, #8832 ) ) ;
#1058=DIRECTION ( 'NONE',  ( 0.000000000000000000, 0.000000000000000000, 1.000000000000000000 ) ) ;
#1080=ORIENTED_EDGE ( 'NONE', *, *, #2708, .F. ) ;
#1100=EDGE_LOOP ( 'NONE', ( #4005, #10378, #7221, #10183 ) ) ;
#1109=DIRECTION ( 'NONE',  ( 0.000000000000000000, 0.000000000000000000, 1.000000000000000000 ) ) ;
#1115=CIRCLE ( 'NONE', #6179, 6.248999999999999666 ) ;
#1123=VECTOR ( 'NONE', #2714, 1000.000000000000000 ) ;
#1129=ADVANCED_FACE ( 'NONE', ( #1340 ), #2146, .T. ) ;
#1136=EDGE_LOOP ( 'NONE', ( #3793, #943, #1240, #4213 ) ) ;
#1153=ORIENTED_EDGE ( 'NONE', *, *, #4265, .F. ) ;
#1154=LINE ( 'NONE', #10030, #1441 ) ;
#1170=DIRECTION ( 'NONE',  ( -1.000000000000000000, 0.000000000000000000, -0.000000000000000000 ) ) ;
#1172=COLOUR_RGB ( '', 0.09019608, 0.27058824, 0.51372549) ;
#1180=ORIENTED_EDGE ( 'NONE', *, *, #6685, .T. ) ;
#1184=CARTESIAN_POINT ( 'NONE',  ( 10.00000000000000000, -7.009698679648292519, 0.7308381473896652381 ) ) ;
#1193=ORIENTED_EDGE ( 'NONE', *, *, #529, .T. ) ;
#1199=DIRECTION ( 'NONE',  ( -1.000000000000000000, -0.000000000000000000, -0.000000000000000000 ) ) ;
#1200=AXIS2_PLACEMENT_3D ( 'NONE', #6027, #9278, #2017 ) ;
#1209=UNCERTAINTY_MEASURE_WITH_UNIT (LENGTH_MEASURE( 1.000000000000000082E-05 ), #6662, 'distance_accuracy_value', 'NONE');
#1210=SURFACE_STYLE_FILL_AREA ( #5126 ) ;
#1214=ORIENTED_EDGE ( 'NONE', *, *, #9476, .T. ) ;
#1215=CYLINDRICAL_SURFACE ( 'NONE', #5234, 2.000000000000000000 ) ;
#1217=CARTESIAN_POINT ( 'NONE',  ( 8.000000000000001776, 0.000000000000000000, 0.000000000000000000 ) ) ;
#1224=CARTESIAN_POINT ( 'NONE',  ( -2.000000000000000000, 8.265874651078044977, -1.981241088980697729 ) ) ;
#1227=DIRECTION ( 'NONE',  ( -1.000000000000000000, -0.000000000000000000, -0.000000000000000000 ) ) ;
#1233=ORIENTED_EDGE ( 'NONE', *, *, #6350, .F. ) ;
#1234=CIRCLE ( 'NONE', #1746, 3.000000000000000000 ) ;
#1237=CARTESIAN_POINT ( 'NONE',  ( -10.00000000000000000, 0.000000000000000000, 0.000000000000000000 ) ) ;
#1239=DIRECTION ( 'NONE',  ( 0.000000000000000000, 0.000000000000000000, 1.000000000000000000 ) ) ;
#1240=ORIENTED_EDGE ( 'NONE', *, *, #2513, .F. ) ;
#1247=EDGE_CURVE ( 'NONE', #1286, #8006, #1362, .T. ) ;
#1249=ORIENTED_EDGE ( 'NONE', *, *, #4265, .T. ) ;
#1270=VECTOR ( 'NONE', #8747, 1000.000000000000000 ) ;
#1271=CARTESIAN_POINT ( 'NONE',  ( 10.00000000000000000, 0.000000000000000000, 0.000000000000000000 ) ) ;
#1286=VERTEX_POINT ( 'NONE', #2412 ) ;
#1290=CARTESIAN_POINT ( 'NONE',  ( -10.00000000000000000, 0.000000000000000000, 0.000000000000000000 ) ) ;
#1305=DIRECTION ( 'NONE',  ( 0.000000000000000000, -3.819167204710539130E-14, -1.000000000000000000 ) ) ;
#1307=DIRECTION ( 'NONE',  ( -1.000000000000000000, -0.000000000000000000, 0.000000000000000000 ) ) ;
#1318=ORIENTED_EDGE ( 'NONE', *, *, #8066, .T. ) ;
#1321=CARTESIAN_POINT ( 'NONE',  ( 10.00000000000000000, 4.058600654062950674, -7.468451026206158083 ) ) ;
#1322=DIRECTION ( 'NONE',  ( 0.000000000000000000, 0.000000000000000000, 1.000000000000000000 ) ) ;
#1325=DIRECTION ( 'NONE',  ( -1.000000000000000000, -0.000000000000000000, -0.000000000000000000 ) ) ;
#1326=CARTESIAN_POINT ( 'NONE',  ( 10.00000000000000000, 6.226349476952025341, 0.5315761383463611933 ) ) ;
#1336=CARTESIAN_POINT ( 'NONE',  ( -10.00000000000000000, 0.000000000000000000, 0.000000000000000000 ) ) ;
#1340=FACE_OUTER_BOUND ( 'NONE', #10401, .T. ) ;
#1342=DIRECTION ( 'NONE',  ( 0.000000000000000000, 0.000000000000000000, 1.000000000000000000 ) ) ;
#1348=EDGE_CURVE ( 'NONE', #8006, #5739, #10016, .T. ) ;
#1353=ORIENTED_EDGE ( 'NONE', *, *, #10459, .T. ) ;
#1362=CIRCLE ( 'NONE', #3407, 3.000000000000000000 ) ;
#1368=DIRECTION ( 'NONE',  ( -1.000000000000000000, -0.000000000000000000, 0.000000000000000000 ) ) ;
#1376=AXIS2_PLACEMENT_3D ( 'NONE', #1728, #978, #2674 ) ;
#1382=DIRECTION ( 'NONE',  ( -1.000000000000000000, -0.000000000000000000, -0.000000000000000000 ) ) ;
#1383=LINE ( 'NONE', #6299, #282 ) ;
#1392=CYLINDRICAL_SURFACE ( 'NONE', #10177, 8.500000000000000000 ) ;
#1394=CYLINDRICAL_SURFACE ( 'NONE', #8064, 8.500000000000000000 ) ;
#1397=( LENGTH_UNIT ( ) NAMED_UNIT ( * ) SI_UNIT ( .MILLI., .METRE. ) );
#1401=ORIENTED_EDGE ( 'NONE', *, *, #4133, .T. ) ;
#1404=AXIS2_PLACEMENT_3D ( 'NONE', #4665, #5463, #4716 ) ;
#1405=DIRECTION ( 'NONE',  ( -1.000000000000000000, -0.000000000000000000, -0.000000000000000000 ) ) ;
#1414=CIRCLE ( 'NONE', #1929, 2.000000000000000000 ) ;
#1426=FACE_OUTER_BOUND ( 'NONE', #4809, .T. ) ;
#1429=CYLINDRICAL_SURFACE ( 'NONE', #3794, 3.000000000000000000 ) ;
#1431=CARTESIAN_POINT ( 'NONE',  ( -2.000000000000000000, -5.979767908488852868, 1.814490771706165351 ) ) ;
#1441=VECTOR ( 'NONE', #6873, 1000.000000000000000 ) ;
#1449=VERTEX_POINT ( 'NONE', #8386 ) ;
#1457=ORIENTED_EDGE ( 'NONE', *, *, #4549, .T. ) ;
#1460=CIRCLE ( 'NONE', #3325, 6.248999999999999666 ) ;
#1461=DIRECTION ( 'NONE',  ( -1.000000000000000000, -0.000000000000000000, -0.000000000000000000 ) ) ;
#1463=ORIENTED_EDGE ( 'NONE', *, *, #328, .T. ) ;
#1466=DIRECTION ( 'NONE',  ( -1.000000000000000000, -0.000000000000000000, -0.000000000000000000 ) ) ;
#1473=DIRECTION ( 'NONE',  ( -1.000000000000000000, -0.000000000000000000, -0.000000000000000000 ) ) ;
#1482=CARTESIAN_POINT ( 'NONE',  ( 10.00000000000000000, 0.000000000000000000, 0.000000000000000000 ) ) ;
#1485=CARTESIAN_POINT ( 'NONE',  ( -2.000000000000001776, 2.449293598294706414E-16, -2.000000000000000000 ) ) ;
#1489=CARTESIAN_POINT ( 'NONE',  ( 10.00000000000000000, 7.008469740302810891, -0.7425307242147085596 ) ) ;
#1495=CARTESIAN_POINT ( 'NONE',  ( 8.000000000000001776, -5.233522515400119701, 4.720195129223260899 ) ) ;
#1496=ORIENTED_EDGE ( 'NONE', *, *, #1047, .F. ) ;
#1507=DIRECTION ( 'NONE',  ( -1.000000000000000000, -0.000000000000000000, -0.000000000000000000 ) ) ;
#1513=ORIENTED_EDGE ( 'NONE', *, *, #7264, .T. ) ;
#1522=ORIENTED_EDGE ( 'NONE', *, *, #253, .T. ) ;
#1531=CARTESIAN_POINT ( 'NONE',  ( 10.00000000000000000, -1.471047635026825784, -6.892461014225975013 ) ) ;
#1540=DIRECTION ( 'NONE',  ( -1.000000000000000000, -0.000000000000000000, 0.000000000000000000 ) ) ;
#1542=ORIENTED_EDGE ( 'NONE', *, *, #8446, .T. ) ;
#1545=AXIS2_PLACEMENT_3D ( 'NONE', #883, #8149, #6541 ) ;
#1558=ORIENTED_EDGE ( 'NONE', *, *, #382, .T. ) ;
#1562=CARTESIAN_POINT ( 'NONE',  ( -10.00000000000000000, 0.000000000000000000, 0.000000000000000000 ) ) ;
#1567=ADVANCED_FACE ( 'NONE', ( #2760 ), #5974, .T. ) ;
#1581=CARTESIAN_POINT ( 'NONE',  ( 10.00000000000000000, 0.000000000000000000, 0.000000000000000000 ) ) ;
#1585=AXIS2_PLACEMENT_3D ( 'NONE', #5606, #10454, #8060 ) ;
#1602=DIRECTION ( 'NONE',  ( -1.000000000000000000, -0.000000000000000000, -0.000000000000000000 ) ) ;
#1613=EDGE_CURVE ( 'NONE', #7025, #5618, #2385, .T. ) ;
#1614=DIRECTION ( 'NONE',  ( -1.000000000000000000, 0.000000000000000000, 0.000000000000000000 ) ) ;
#1622=DIRECTION ( 'NONE',  ( 0.000000000000000000, 0.000000000000000000, -1.000000000000000000 ) ) ;
#1626=ORIENTED_EDGE ( 'NONE', *, *, #4152, .F. ) ;
#1627=CIRCLE ( 'NONE', #9936, 3.000000000000000000 ) ;
#1629=DIRECTION ( 'NONE',  ( -1.000000000000000000, -0.000000000000000000, -0.000000000000000000 ) ) ;
#1632=CIRCLE ( 'NONE', #280, 3.000000000000000000 ) ;
#1637=EDGE_CURVE ( 'NONE', #371, #5056, #4240, .T. ) ;
#1641=CARTESIAN_POINT ( 'NONE',  ( 8.000000000000001776, 5.471841788314748989, -3.018103451449677621 ) ) ;
#1645=VERTEX_POINT ( 'NONE', #7039 ) ;
#1646=EDGE_CURVE ( 'NONE', #10253, #5539, #7742, .T. ) ;
#1650=LINE ( 'NONE', #802, #5733 ) ;
#1659=DIRECTION ( 'NONE',  ( -1.000000000000000000, -0.000000000000000000, 0.000000000000000000 ) ) ;
#1671=CARTESIAN_POINT ( 'NONE',  ( -10.00000000000000000, 0.000000000000000000, 0.000000000000000000 ) ) ;
#1679=CIRCLE ( 'NONE', #3204, 8.500000000000000000 ) ;
#1681=EDGE_CURVE ( 'NONE', #4156, #3105, #9337, .T. ) ;
#1682=ORIENTED_EDGE ( 'NONE', *, *, #3635, .F. ) ;
#1688=ORIENTED_EDGE ( 'NONE', *, *, #1247, .F. ) ;
#1705=EDGE_LOOP ( 'NONE', ( #9011, #6484, #2571, #8572 ) ) ;
#1709=EDGE_CURVE ( 'NONE', #7874, #8403, #4544, .T. ) ;
#1712=AXIS2_PLACEMENT_3D ( 'NONE', #88, #3363, #9095 ) ;
#1719=CIRCLE ( 'NONE', #8323, 3.000000000000000000 ) ;
#1723=EDGE_CURVE ( 'NONE', #1757, #7886, #4598, .T. ) ;
#1728=CARTESIAN_POINT ( 'NONE',  ( -2.000000000000000000, 0.000000000000000000, 0.000000000000000000 ) ) ;
#1729=DIRECTION ( 'NONE',  ( -1.000000000000000000, -0.000000000000000000, -0.000000000000000000 ) ) ;
#1737=VERTEX_POINT ( 'NONE', #5296 ) ;
#1740=ORIENTED_EDGE ( 'NONE', *, *, #4922, .F. ) ;
#1746=AXIS2_PLACEMENT_3D ( 'NONE', #50, #737, #6289 ) ;
#1751=EDGE_LOOP ( 'NONE', ( #7175, #733, #2152, #6231 ) ) ;
#1757=VERTEX_POINT ( 'NONE', #6883 ) ;
#1758=CARTESIAN_POINT ( 'NONE',  ( 10.00000000000000000, 0.000000000000000000, 0.000000000000000000 ) ) ;
#1764=DIRECTION ( 'NONE',  ( -1.000000000000000000, -0.000000000000000000, 0.000000000000000000 ) ) ;
#1766=DIRECTION ( 'NONE',  ( 0.000000000000000000, 0.000000000000000000, 1.000000000000000000 ) ) ;
#1777=VERTEX_POINT ( 'NONE', #6063 ) ;
#1780=FACE_OUTER_BOUND ( 'NONE', #1705, .T. ) ;
#1788=DIRECTION ( 'NONE',  ( -0.000000000000000000, 0.000000000000000000, 1.000000000000000000 ) ) ;
#1791=EDGE_LOOP ( 'NONE', ( #4232, #4106, #4971, #10229 ) ) ;
#1798=ORIENTED_EDGE ( 'NONE', *, *, #4717, .F. ) ;
#1801=AXIS2_PLACEMENT_3D ( 'NONE', #73, #2664, #1766 ) ;
#1804=LINE ( 'NONE', #5030, #2388 ) ;
#1809=EDGE_CURVE ( 'NONE', #4861, #5471, #195, .T. ) ;
#1830=VERTEX_POINT ( 'NONE', #6122 ) ;
#1838=ADVANCED_FACE ( 'NONE', ( #6916 ), #3691, .T. ) ;
#1841=ORIENTED_EDGE ( 'NONE', *, *, #4751, .F. ) ;
#1848=ORIENTED_EDGE ( 'NONE', *, *, #5300, .T. ) ;
#1851=SHAPE_REPRESENTATION_RELATIONSHIP ( 'NONE' , 'NONE' ,  #8347, #689 ) ;
#1853=ORIENTED_EDGE ( 'NONE', *, *, #7768, .F. ) ;
#1854=CARTESIAN_POINT ( 'NONE',  ( 10.00000000000000000, -5.979767908488829775, -1.814490771706245065 ) ) ;
#1864=CIRCLE ( 'NONE', #3879, 6.248999999999999666 ) ;
#1872=CARTESIAN_POINT ( 'NONE',  ( 10.00000000000000000, -5.349675154362301122, -3.229702268444983648 ) ) ;
#1882=DIRECTION ( 'NONE',  ( 0.000000000000000000, 0.000000000000000000, 1.000000000000000000 ) ) ;
#1883=CIRCLE ( 'NONE', #8988, 8.500000000000000000 ) ;
#1904=ORIENTED_EDGE ( 'NONE', *, *, #9554, .F. ) ;
#1907=ORIENTED_EDGE ( 'NONE', *, *, #4497, .F. ) ;
#1912=DIRECTION ( 'NONE',  ( -1.000000000000000000, -0.000000000000000000, -0.000000000000000000 ) ) ;
#1922=DIRECTION ( 'NONE',  ( 0.000000000000000000, 0.000000000000000000, 1.000000000000000000 ) ) ;
#1924=CARTESIAN_POINT ( 'NONE',  ( -2.000000000000000000, 1.693568526656785686E-17, 2.343061888689530026 ) ) ;
#1929=AXIS2_PLACEMENT_3D ( 'NONE', #5827, #7325, #3245 ) ;
#1941=EDGE_LOOP ( 'NONE', ( #4951, #8464, #501, #6269, #6928, #7301, #2227, #4780, #1496, #7452, #395, #571, #9854, #4785, #4974, #3444, #1841, #9369, #3896, #2750, #9597, #5523, #991, #5584, #1688, #4478, #8851, #9373, #1853, #983, #3480, #7131, #3072, #3749, #10331, #5812, #1153, #8634, #4260, #1798, #4184, #8716, #6045, #8263, #10050, #10397 ) ) ;
#1944=VERTEX_POINT ( 'NONE', #8781 ) ;
#1953=ORIENTED_EDGE ( 'NONE', *, *, #3125, .T. ) ;
#1957=EDGE_CURVE ( 'NONE', #4491, #10281, #7132, .T. ) ;
#1958=VERTEX_POINT ( 'NONE', #3060 ) ;
#1977=CARTESIAN_POINT ( 'NONE',  ( -2.000000000000000000, -7.063614741696270016, 0.000000000000000000 ) ) ;
#1987=DIRECTION ( 'NONE',  ( 0.000000000000000000, -8.673617379884032514E-16, -1.000000000000000000 ) ) ;
#1997=EDGE_CURVE ( 'NONE', #9192, #7510, #9589, .T. ) ;
#1998=DIRECTION ( 'NONE',  ( 1.000000000000000000, 0.000000000000000000, 0.000000000000000000 ) ) ;
#2007=EDGE_CURVE ( 'NONE', #8580, #2344, #9689, .T. ) ;
#2008=ORIENTED_EDGE ( 'NONE', *, *, #7002, .T. ) ;
#2017=DIRECTION ( 'NONE',  ( 0.000000000000000000, -4.263256414560601746E-14, -1.000000000000000000 ) ) ;
#2025=DIRECTION ( 'NONE',  ( 0.000000000000000000, 0.000000000000000000, 1.000000000000000000 ) ) ;
#2027=EDGE_CURVE ( 'NONE', #4853, #7886, #6784, .T. ) ;
#2028=AXIS2_PLACEMENT_3D ( 'NONE', #2953, #1466, #1305 ) ;
#2043=AXIS2_PLACEMENT_3D ( 'NONE', #5399, #4503, #8643 ) ;
#2046=VERTEX_POINT ( 'NONE', #3670 ) ;
#2051=DIRECTION ( 'NONE',  ( 0.000000000000000000, 0.000000000000000000, 1.000000000000000000 ) ) ;
#2054=ORIENTED_EDGE ( 'NONE', *, *, #3622, .F. ) ;
#2061=UNCERTAINTY_MEASURE_WITH_UNIT (LENGTH_MEASURE( 1.000000000000000082E-05 ), #1397, 'distance_accuracy_value', 'NONE');
#2067=DIRECTION ( 'NONE',  ( 0.000000000000000000, 0.000000000000000000, 1.000000000000000000 ) ) ;
#2068=CARTESIAN_POINT ( 'NONE',  ( -2.000000000000000000, -6.200809695932781196, 0.7745709230444935978 ) ) ;
#2085=AXIS2_PLACEMENT_3D ( 'NONE', #4386, #7632, #2808 ) ;
#2086=ADVANCED_FACE ( 'NONE', ( #8556 ), #2142, .T. ) ;
#2089=DIRECTION ( 'NONE',  ( -1.000000000000000000, -0.000000000000000000, -0.000000000000000000 ) ) ;
#2099=ADVANCED_FACE ( 'NONE', ( #6042 ), #6258, .F. ) ;
#2101=AXIS2_PLACEMENT_3D ( 'NONE', #7090, #5610, #4547 ) ;
#2102=DIRECTION ( 'NONE',  ( 0.000000000000000000, 0.000000000000000000, 1.000000000000000000 ) ) ;
#2104=ORIENTED_EDGE ( 'NONE', *, *, #2718, .F. ) ;
#2116=ORIENTED_EDGE ( 'NONE', *, *, #8726, .T. ) ;
#2117=DIRECTION ( 'NONE',  ( -1.000000000000000000, 0.000000000000000000, 0.000000000000000000 ) ) ;
#2121=VECTOR ( 'NONE', #9568, 1000.000000000000000 ) ;
#2122=DIRECTION ( 'NONE',  ( 0.000000000000000000, 0.000000000000000000, 1.000000000000000000 ) ) ;
#2125=CARTESIAN_POINT ( 'NONE',  ( 8.000000000000001776, 0.000000000000000000, 0.000000000000000000 ) ) ;
#2139=VECTOR ( 'NONE', #60, 1000.000000000000000 ) ;
#2142=CYLINDRICAL_SURFACE ( 'NONE', #5601, 8.500000000000000000 ) ;
#2146=CYLINDRICAL_SURFACE ( 'NONE', #6744, 3.000000000000000000 ) ;
#2152=ORIENTED_EDGE ( 'NONE', *, *, #1646, .F. ) ;
#2154=DIRECTION ( 'NONE',  ( 0.000000000000000000, 0.000000000000000000, 1.000000000000000000 ) ) ;
#2162=VERTEX_POINT ( 'NONE', #3037 ) ;
#2170=ORIENTED_EDGE ( 'NONE', *, *, #382, .F. ) ;
#2180=DIRECTION ( 'NONE',  ( -1.000000000000000000, 0.000000000000000000, 0.000000000000000000 ) ) ;
#2197=DIRECTION ( 'NONE',  ( -1.000000000000000000, -0.000000000000000000, 0.000000000000000000 ) ) ;
#2201=ORIENTED_EDGE ( 'NONE', *, *, #427, .F. ) ;
#2203=CARTESIAN_POINT ( 'NONE',  ( -2.000000000000000000, 0.000000000000000000, 0.000000000000000000 ) ) ;
#2207=VERTEX_POINT ( 'NONE', #2935 ) ;
#2212=AXIS2_PLACEMENT_3D ( 'NONE', #6373, #9626, #8030 ) ;
#2221=CARTESIAN_POINT ( 'NONE',  ( 10.00000000000000000, -7.851777359434023218, 3.255701506262409506 ) ) ;
#2224=CARTESIAN_POINT ( 'NONE',  ( 10.00000000000000000, 0.000000000000000000, 0.000000000000000000 ) ) ;
#2225=DIRECTION ( 'NONE',  ( -1.000000000000000000, -0.000000000000000000, -0.000000000000000000 ) ) ;
#2227=ORIENTED_EDGE ( 'NONE', *, *, #5179, .F. ) ;
#2231=FACE_OUTER_BOUND ( 'NONE', #10112, .T. ) ;
#2263=CARTESIAN_POINT ( 'NONE',  ( 10.00000000000000000, 0.000000000000000000, 0.000000000000000000 ) ) ;
#2265=EDGE_CURVE ( 'NONE', #4339, #8766, #9683, .T. ) ;
#2275=CIRCLE ( 'NONE', #2085, 8.500000000000000000 ) ;
#2283=CARTESIAN_POINT ( 'NONE',  ( 8.000000000000001776, -1.179494851233864106, -6.136676046192498291 ) ) ;
#2290=PRODUCT_DEFINITION_FORMATION_WITH_SPECIFIED_SOURCE ( 'ANY', '', #10292, .NOT_KNOWN. ) ;
#2303=SURFACE_STYLE_USAGE ( .BOTH. , #7008 ) ;
#2317=DIRECTION ( 'NONE',  ( -1.000000000000000000, -0.000000000000000000, -0.000000000000000000 ) ) ;
#2326=EDGE_CURVE ( 'NONE', #5471, #9996, #6564, .T. ) ;
#2329=ORIENTED_EDGE ( 'NONE', *, *, #2530, .T. ) ;
#2339=LINE ( 'NONE', #5616, #4545 ) ;
#2343=CYLINDRICAL_SURFACE ( 'NONE', #3104, 3.000000000000000000 ) ;
#2344=VERTEX_POINT ( 'NONE', #58 ) ;
#2359=VECTOR ( 'NONE', #8860, 1000.000000000000000 ) ;
#2361=EDGE_LOOP ( 'NONE', ( #7769, #7206, #1682, #7238 ) ) ;
#2364=FACE_OUTER_BOUND ( 'NONE', #153, .T. ) ;
#2366=CARTESIAN_POINT ( 'NONE',  ( 10.00000000000000000, 8.265874651078044977, -1.981241088980697729 ) ) ;
#2369=DIRECTION ( 'NONE',  ( -1.000000000000000000, -0.000000000000000000, 0.000000000000000000 ) ) ;
#2373=CIRCLE ( 'NONE', #4055, 3.000000000000000000 ) ;
#2374=CARTESIAN_POINT ( 'NONE',  ( -2.000000000000001776, 0.000000000000000000, 2.000000000000000000 ) ) ;
#2375=CIRCLE ( 'NONE', #10336, 8.500000000000000000 ) ;
#2379=DIRECTION ( 'NONE',  ( -1.000000000000000000, 0.000000000000000000, -0.000000000000000000 ) ) ;
#2385=CIRCLE ( 'NONE', #1200, 8.500000000000000000 ) ;
#2388=VECTOR ( 'NONE', #7826, 1000.000000000000000 ) ;
#2396=DIRECTION ( 'NONE',  ( -1.000000000000000000, -0.000000000000000000, -0.000000000000000000 ) ) ;
#2402=CARTESIAN_POINT ( 'NONE',  ( -2.000000000000000000, 8.265874651078018331, 1.981241088980807419 ) ) ;
#2403=EDGE_CURVE ( 'NONE', #6339, #1944, #112, .T. ) ;
#2409=DIRECTION ( 'NONE',  ( -1.000000000000000000, -0.000000000000000000, -0.000000000000000000 ) ) ;
#2410=DIRECTION ( 'NONE',  ( 0.000000000000000000, 0.000000000000000000, 1.000000000000000000 ) ) ;
#2412=CARTESIAN_POINT ( 'NONE',  ( 10.00000000000000000, -1.179494851233864106, -6.136676046192498291 ) ) ;
#2413=CARTESIAN_POINT ( 'NONE',  ( 10.00000000000000000, 8.357095590591340439, 1.552080310331536372 ) ) ;
#2426=VERTEX_POINT ( 'NONE', #3631 ) ;
#2428=EDGE_CURVE ( 'NONE', #9050, #1645, #1804, .T. ) ;
#2431=AXIS2_PLACEMENT_3D ( 'NONE', #430, #3659, #4601 ) ;
#2436=CARTESIAN_POINT ( 'NONE',  ( -2.000000000000000000, -7.063614741696270016, 3.730353617970412206 ) ) ;
#2449=DIRECTION ( 'NONE',  ( -1.000000000000000000, -0.000000000000000000, -0.000000000000000000 ) ) ;
#2456=PRODUCT_CONTEXT ( 'NONE', #10355, 'mechanical' ) ;
#2461=CARTESIAN_POINT ( 'NONE',  ( 10.00000000000000000, -3.573533178329545645, -5.126388750707257635 ) ) ;
#2472=CARTESIAN_POINT ( 'NONE',  ( 4.000000000000000888, 1.106368468154538931, -8.427689411260562480 ) ) ;
#2475=CIRCLE ( 'NONE', #4659, 3.000000000000000000 ) ;
#2477=EDGE_CURVE ( 'NONE', #7886, #9192, #1719, .T. ) ;
#2481=VECTOR ( 'NONE', #5979, 1000.000000000000000 ) ;
#2484=CARTESIAN_POINT ( 'NONE',  ( -2.000000000000000000, 6.226349476952025341, 0.5315761383463611933 ) ) ;
#2496=CARTESIAN_POINT ( 'NONE',  ( -2.000000000000000000, 0.000000000000000000, 0.000000000000000000 ) ) ;
#2506=CYLINDRICAL_SURFACE ( 'NONE', #6507, 3.000000000000000000 ) ;
#2513=EDGE_CURVE ( 'NONE', #5181, #7025, #6115, .T. ) ;
#2517=ORIENTED_EDGE ( 'NONE', *, *, #3917, .T. ) ;
#2530=EDGE_CURVE ( 'NONE', #5853, #5625, #3442, .T. ) ;
#2535=AXIS2_PLACEMENT_3D ( 'NONE', #3543, #1912, #9329 ) ;
#2544=ADVANCED_FACE ( 'NONE', ( #9424 ), #9366, .T. ) ;
#2546=CYLINDRICAL_SURFACE ( 'NONE', #90, 3.000000000000000000 ) ;
#2554=VECTOR ( 'NONE', #4552, 1000.000000000000000 ) ;
#2562=APPLICATION_CONTEXT ( 'automotive_design' ) ;
#2563=CARTESIAN_POINT ( 'NONE',  ( -2.000000000000000000, 8.357095590591340439, -1.552080310331536372 ) ) ;
#2564=DIRECTION ( 'NONE',  ( -1.000000000000000000, -0.000000000000000000, -0.000000000000000000 ) ) ;
#2565=CARTESIAN_POINT ( 'NONE',  ( -2.000000000000000000, 1.106368468154538931, -8.427689411260562480 ) ) ;
#2566=CARTESIAN_POINT ( 'NONE',  ( -2.000000000000000000, -5.233522515400054864, -4.720195129223331065 ) ) ;
#2570=DIRECTION ( 'NONE',  ( 0.000000000000000000, 0.000000000000000000, 1.000000000000000000 ) ) ;
#2571=ORIENTED_EDGE ( 'NONE', *, *, #671, .F. ) ;
#2599=DIRECTION ( 'NONE',  ( -1.000000000000000000, 0.000000000000000000, -0.000000000000000000 ) ) ;
#2602=ORIENTED_EDGE ( 'NONE', *, *, #4777, .F. ) ;
#2603=DIRECTION ( 'NONE',  ( 0.000000000000000000, 0.000000000000000000, 1.000000000000000000 ) ) ;
#2614=CYLINDRICAL_SURFACE ( 'NONE', #7378, 3.000000000000000000 ) ;
#2615=FACE_OUTER_BOUND ( 'NONE', #4464, .T. ) ;
#2616=DIRECTION ( 'NONE',  ( 0.000000000000000000, 1.000000000000000000, -7.228014483236698281E-18 ) ) ;
#2622=DIRECTION ( 'NONE',  ( 0.000000000000000000, 0.000000000000000000, 1.000000000000000000 ) ) ;
#2623=ORIENTED_EDGE ( 'NONE', *, *, #2428, .T. ) ;
#2626=PLANE ( 'NONE',  #1712 ) ;
#2644=VERTEX_POINT ( 'NONE', #3208 ) ;
#2649=CARTESIAN_POINT ( 'NONE',  ( 10.00000000000000000, 7.003298780661491918, -4.817032923780498521 ) ) ;
#2651=DIRECTION ( 'NONE',  ( -1.000000000000000000, 0.000000000000000000, -0.000000000000000000 ) ) ;
#2657=ORIENTED_EDGE ( 'NONE', *, *, #5102, .T. ) ;
#2664=DIRECTION ( 'NONE',  ( -1.000000000000000000, -0.000000000000000000, 0.000000000000000000 ) ) ;
#2665=DIRECTION ( 'NONE',  ( 0.000000000000000000, 0.000000000000000000, -1.000000000000000000 ) ) ;
#2669=CARTESIAN_POINT ( 'NONE',  ( 10.00000000000000000, 7.008469740302810891, -0.7425307242147085596 ) ) ;
#2674=DIRECTION ( 'NONE',  ( 0.000000000000000000, 8.881784197001252323E-16, -1.000000000000000000 ) ) ;
#2691=ORIENTED_EDGE ( 'NONE', *, *, #8760, .F. ) ;
#2694=EDGE_LOOP ( 'NONE', ( #8630, #5482, #9256, #6327 ) ) ;
#2696=VECTOR ( 'NONE', #2754, 1000.000000000000000 ) ;
#2708=EDGE_CURVE ( 'NONE', #5056, #1737, #6433, .T. ) ;
#2713=CIRCLE ( 'NONE', #9322, 6.248999999999999666 ) ;
#2714=DIRECTION ( 'NONE',  ( -1.000000000000000000, 0.000000000000000000, 0.000000000000000000 ) ) ;
#2718=EDGE_CURVE ( 'NONE', #8842, #1757, #7122, .T. ) ;
#2727=CIRCLE ( 'NONE', #10351, 3.000000000000000888 ) ;
#2733=EDGE_CURVE ( 'NONE', #7510, #1757, #6609, .T. ) ;
#2734=EDGE_CURVE ( 'NONE', #145, #1958, #7815, .T. ) ;
#2748=EDGE_CURVE ( 'NONE', #5539, #4283, #9339, .T. ) ;
#2750=ORIENTED_EDGE ( 'NONE', *, *, #9279, .F. ) ;
#2754=DIRECTION ( 'NONE',  ( 1.000000000000000000, -0.000000000000000000, -0.000000000000000000 ) ) ;
#2760=FACE_OUTER_BOUND ( 'NONE', #8587, .T. ) ;
#2762=DIRECTION ( 'NONE',  ( -1.000000000000000000, -0.000000000000000000, 0.000000000000000000 ) ) ;
#2764=VECTOR ( 'NONE', #1540, 1000.000000000000000 ) ;
#2774=ORIENTED_EDGE ( 'NONE', *, *, #8236, .T. ) ;
#2776=DIRECTION ( 'NONE',  ( 1.000000000000000000, 0.000000000000000000, 0.000000000000000000 ) ) ;
#2780=AXIS2_PLACEMENT_3D ( 'NONE', #5396, #4602, #8692 ) ;
#2792=EDGE_CURVE ( 'NONE', #5123, #2426, #7305, .T. ) ;
#2801=EDGE_CURVE ( 'NONE', #4853, #8842, #7343, .T. ) ;
#2808=DIRECTION ( 'NONE',  ( 0.000000000000000000, 2.486899575160350966E-14, -1.000000000000000000 ) ) ;
#2812=AXIS2_PLACEMENT_3D ( 'NONE', #9834, #2564, #5778 ) ;
#2815=LINE ( 'NONE', #6781, #5977 ) ;
#2820=DIRECTION ( 'NONE',  ( 0.000000000000000000, 0.000000000000000000, 1.000000000000000000 ) ) ;
#2828=AXIS2_PLACEMENT_3D ( 'NONE', #5097, #9941, #2665 ) ;
#2848=ORIENTED_EDGE ( 'NONE', *, *, #10393, .T. ) ;
#2850=LINE ( 'NONE', #5182, #4651 ) ;
#2853=DIRECTION ( 'NONE',  ( -1.000000000000000000, 0.000000000000000000, -0.000000000000000000 ) ) ;
#2854=DIRECTION ( 'NONE',  ( 0.000000000000000000, -1.598721155460225418E-14, -1.000000000000000000 ) ) ;
#2866=AXIS2_PLACEMENT_3D ( 'NONE', #981, #8934, #10494 ) ;
#2867=CYLINDRICAL_SURFACE ( 'NONE', #4713, 3.000000000000000000 ) ;
#2875=VECTOR ( 'NONE', #6047, 1000.000000000000000 ) ;
#2880=CARTESIAN_POINT ( 'NONE',  ( 10.00000000000000000, -8.497168642645963388, -0.2193742428685764301 ) ) ;
#2881=ORIENTED_EDGE ( 'NONE', *, *, #8613, .T. ) ;
#2895=CARTESIAN_POINT ( 'NONE',  ( 10.00000000000000000, -2.417132211460011337, -8.149077976821821778 ) ) ;
#2899=AXIS2_PLACEMENT_3D ( 'NONE', #1671, #3263, #1882 ) ;
#2900=LINE ( 'NONE', #3741, #5744 ) ;
#2901=EDGE_LOOP ( 'NONE', ( #1740, #9429 ) ) ;
#2904=ORIENTED_EDGE ( 'NONE', *, *, #926, .F. ) ;
#2905=ADVANCED_FACE ( 'NONE', ( #5051 ), #1031, .T. ) ;
#2907=SURFACE_SIDE_STYLE ('',( #1210 ) ) ;
#2913=EDGE_CURVE ( 'NONE', #1944, #8403, #3361, .T. ) ;
#2920=DIRECTION ( 'NONE',  ( -1.000000000000000000, -0.000000000000000000, -0.000000000000000000 ) ) ;
#2923=CARTESIAN_POINT ( 'NONE',  ( 50.00005079999999680, 0.000000000000000000, 0.000000000000000000 ) ) ;
#2933=DIRECTION ( 'NONE',  ( 1.000000000000000000, 0.000000000000000000, 0.000000000000000000 ) ) ;
#2935=CARTESIAN_POINT ( 'NONE',  ( 10.00000000000000000, 3.771202944355774189, -4.982773259188334691 ) ) ;
#2941=AXIS2_PLACEMENT_3D ( 'NONE', #2970, #4653, #632 ) ;
#2951=EDGE_LOOP ( 'NONE', ( #673, #7930 ) ) ;
#2953=CARTESIAN_POINT ( 'NONE',  ( -2.000000000000000000, 0.000000000000000000, 0.000000000000000000 ) ) ;
#2963=CIRCLE ( 'NONE', #2828, 6.248999999999999666 ) ;
#2970=CARTESIAN_POINT ( 'NONE',  ( 8.000000000000001776, 0.000000000000000000, 0.000000000000000000 ) ) ;
#2974=AXIS2_PLACEMENT_3D ( 'NONE', #9218, #3747, #10129 ) ;
#2985=AXIS2_PLACEMENT_3D ( 'NONE', #5932, #330, #2820 ) ;
#2986=EDGE_CURVE ( 'NONE', #4320, #10319, #8330, .T. ) ;
#2988=DIRECTION ( 'NONE',  ( 0.000000000000000000, 0.000000000000000000, 1.000000000000000000 ) ) ;
#2993=DIRECTION ( 'NONE',  ( -1.000000000000000000, -0.000000000000000000, -0.000000000000000000 ) ) ;
#3015=CARTESIAN_POINT ( 'NONE',  ( 8.000000000000001776, 0.000000000000000000, 0.000000000000000000 ) ) ;
#3019=DIRECTION ( 'NONE',  ( -1.000000000000000000, -0.000000000000000000, 0.000000000000000000 ) ) ;
#3025=CARTESIAN_POINT ( 'NONE',  ( -2.000000000000000000, 0.000000000000000000, 0.000000000000000000 ) ) ;
#3028=CIRCLE ( 'NONE', #9128, 3.000000000000000000 ) ;
#3034=EDGE_CURVE ( 'NONE', #5902, #10253, #1115, .T. ) ;
#3037=CARTESIAN_POINT ( 'NONE',  ( -2.000000000000000000, 7.008469740302810891, 2.257469275785291440 ) ) ;
#3040=CARTESIAN_POINT ( 'NONE',  ( 10.00000000000000000, 8.265874651078018331, 1.981241088980807419 ) ) ;
#3042=AXIS2_PLACEMENT_3D ( 'NONE', #2566, #7977, #5575 ) ;
#3060=CARTESIAN_POINT ( 'NONE',  ( -2.000000000000000000, -5.848742439617878652, -6.167836887841048110 ) ) ;
#3063=EDGE_LOOP ( 'NONE', ( #7234, #9246, #6794, #2104 ) ) ;
#3064=CARTESIAN_POINT ( 'NONE',  ( 8.000000000000001776, 0.000000000000000000, 0.000000000000000000 ) ) ;
#3072=ORIENTED_EDGE ( 'NONE', *, *, #3676, .F. ) ;
#3076=CARTESIAN_POINT ( 'NONE',  ( 10.00000000000000000, -7.063614741696270016, 2.343061888689530026 ) ) ;
#3081=CARTESIAN_POINT ( 'NONE',  ( 8.000000000000001776, 2.871924938129970517, -6.435996203144478400 ) ) ;
#3094=( NAMED_UNIT ( * ) SI_UNIT ( $, .STERADIAN. ) SOLID_ANGLE_UNIT ( ) );
#3104=AXIS2_PLACEMENT_3D ( 'NONE', #1495, #10475, #8077 ) ;
#3105=VERTEX_POINT ( 'NONE', #7598 ) ;
#3112=ADVANCED_FACE ( 'NONE', ( #3671 ), #344, .T. ) ;
#3118=DIRECTION ( 'NONE',  ( 0.000000000000000000, 2.602085213965210642E-15, -1.000000000000000000 ) ) ;
#3125=EDGE_CURVE ( 'NONE', #7252, #4491, #1627, .T. ) ;
#3128=CARTESIAN_POINT ( 'NONE',  ( 10.00000000000000000, -2.834406817834849601, -8.013497238472808704 ) ) ;
#3145=CYLINDRICAL_SURFACE ( 'NONE', #2212, 6.248999999999999666 ) ;
#3155=ORIENTED_EDGE ( 'NONE', *, *, #1957, .F. ) ;
#3166=ORIENTED_EDGE ( 'NONE', *, *, #4976, .F. ) ;
#3175=ADVANCED_FACE ( 'NONE', ( #3995 ), #1394, .T. ) ;
#3182=CARTESIAN_POINT ( 'NONE',  ( 4.000000000000000888, -2.834406817834849601, -8.013497238472808704 ) ) ;
#3191=CYLINDRICAL_SURFACE ( 'NONE', #1404, 3.000000000000000000 ) ;
#3197=DIRECTION ( 'NONE',  ( 1.000000000000000000, 0.000000000000000000, -0.000000000000000000 ) ) ;
#3204=AXIS2_PLACEMENT_3D ( 'NONE', #4086, #2396, #4825 ) ;
#3206=AXIS2_PLACEMENT_3D ( 'NONE', #6980, #5548, #10184 ) ;
#3208=CARTESIAN_POINT ( 'NONE',  ( -2.000000000000000000, -8.497168642645966941, 0.2193742428684610779 ) ) ;
#3211=DIRECTION ( 'NONE',  ( 1.000000000000000000, 0.000000000000000000, 0.000000000000000000 ) ) ;
#3219=CARTESIAN_POINT ( 'NONE',  ( -2.000000000000000000, -7.009698679648292519, 0.7308381473896652381 ) ) ;
#3229=VECTOR ( 'NONE', #631, 1000.000000000000000 ) ;
#3231=VECTOR ( 'NONE', #2651, 1000.000000000000000 ) ;
#3245=DIRECTION ( 'NONE',  ( 0.000000000000000000, 0.000000000000000000, 1.000000000000000000 ) ) ;
#3263=DIRECTION ( 'NONE',  ( -1.000000000000000000, -0.000000000000000000, -0.000000000000000000 ) ) ;
#3264=CARTESIAN_POINT ( 'NONE',  ( -10.00000000000000000, 0.000000000000000000, 0.000000000000000000 ) ) ;
#3272=EDGE_CURVE ( 'NONE', #5618, #837, #7817, .T. ) ;
#3287=DIRECTION ( 'NONE',  ( 0.000000000000000000, 0.000000000000000000, 1.000000000000000000 ) ) ;
#3288=CARTESIAN_POINT ( 'NONE',  ( 10.00000000000000000, 0.000000000000000000, 0.000000000000000000 ) ) ;
#3289=LINE ( 'NONE', #8072, #2359 ) ;
#3291=ORIENTED_EDGE ( 'NONE', *, *, #3658, .T. ) ;
#3301=DIRECTION ( 'NONE',  ( -1.000000000000000000, 0.000000000000000000, -0.000000000000000000 ) ) ;
#3304=DIRECTION ( 'NONE',  ( -1.000000000000000000, 0.000000000000000000, 0.000000000000000000 ) ) ;
#3305=DIRECTION ( 'NONE',  ( -1.000000000000000000, -0.000000000000000000, -0.000000000000000000 ) ) ;
#3314=CYLINDRICAL_SURFACE ( 'NONE', #9167, 3.000000000000000000 ) ;
#3315=ORIENTED_EDGE ( 'NONE', *, *, #8174, .T. ) ;
#3318=DIRECTION ( 'NONE',  ( 0.000000000000000000, 0.000000000000000000, -1.000000000000000000 ) ) ;
#3323=CIRCLE ( 'NONE', #9249, 3.000000000000000000 ) ;
#3325=AXIS2_PLACEMENT_3D ( 'NONE', #3025, #1325, #537 ) ;
#3326=EDGE_LOOP ( 'NONE', ( #3483, #1193, #5703, #1848 ) ) ;
#3342=ORIENTED_EDGE ( 'NONE', *, *, #5687, .F. ) ;
#3356=ADVANCED_FACE ( 'NONE', ( #2615 ), #3409, .F. ) ;
#3361=LINE ( 'NONE', #8147, #7986 ) ;
#3362=ADVANCED_FACE ( 'NONE', ( #4144 ), #8922, .T. ) ;
#3363=DIRECTION ( 'NONE',  ( 0.000000000000000000, -1.000000000000000000, 0.000000000000000000 ) ) ;
#3364=VERTEX_POINT ( 'NONE', #2461 ) ;
#3367=EDGE_LOOP ( 'NONE', ( #2116, #1542, #4704, #757 ) ) ;
#3373=EDGE_CURVE ( 'NONE', #6398, #6869, #2475, .T. ) ;
#3389=FACE_OUTER_BOUND ( 'NONE', #2694, .T. ) ;
#3393=DIRECTION ( 'NONE',  ( 0.000000000000000000, 0.000000000000000000, -1.000000000000000000 ) ) ;
#3402=VECTOR ( 'NONE', #8117, 1000.000000000000000 ) ;
#3407=AXIS2_PLACEMENT_3D ( 'NONE', #6423, #7435, #4999 ) ;
#3408=CYLINDRICAL_SURFACE ( 'NONE', #951, 3.000000000000000000 ) ;
#3409=PLANE ( 'NONE',  #3816 ) ;
#3410=AXIS2_PLACEMENT_3D ( 'NONE', #7068, #1461, #1622 ) ;
#3416=ORIENTED_EDGE ( 'NONE', *, *, #6140, .F. ) ;
#3439=AXIS2_PLACEMENT_3D ( 'NONE', #9383, #8585, #423 ) ;
#3442=LINE ( 'NONE', #6910, #3231 ) ;
#3444=ORIENTED_EDGE ( 'NONE', *, *, #9791, .F. ) ;
#3450=DIRECTION ( 'NONE',  ( 0.000000000000000000, 0.000000000000000000, 1.000000000000000000 ) ) ;
#3457=CARTESIAN_POINT ( 'NONE',  ( -2.000000000000000000, 52.93638525830372998, 0.000000000000000000 ) ) ;
#3462=CIRCLE ( 'NONE', #4276, 3.000000000000000000 ) ;
#3470=ORIENTED_EDGE ( 'NONE', *, *, #2326, .F. ) ;
#3471=AXIS2_PLACEMENT_3D ( 'NONE', #4975, #2599, #1058 ) ;
#3473=CARTESIAN_POINT ( 'NONE',  ( 10.00000000000000000, -7.009698679648282749, -0.7308381473897593850 ) ) ;
#3474=ORIENTED_EDGE ( 'NONE', *, *, #4640, .F. ) ;
#3480=ORIENTED_EDGE ( 'NONE', *, *, #7475, .F. ) ;
#3481=DIRECTION ( 'NONE',  ( 0.000000000000000000, 0.000000000000000000, 1.000000000000000000 ) ) ;
#3483=ORIENTED_EDGE ( 'NONE', *, *, #7262, .T. ) ;
#3489=VECTOR ( 'NONE', #3528, 1000.000000000000000 ) ;
#3491=VECTOR ( 'NONE', #4346, 1000.000000000000000 ) ;
#3495=DIRECTION ( 'NONE',  ( 0.000000000000000000, 0.000000000000000000, -1.000000000000000000 ) ) ;
#3498=EDGE_CURVE ( 'NONE', #4944, #371, #7380, .T. ) ;
#3506=FACE_OUTER_BOUND ( 'NONE', #4266, .T. ) ;
#3526=ORIENTED_EDGE ( 'NONE', *, *, #4408, .T. ) ;
#3528=DIRECTION ( 'NONE',  ( -1.000000000000000000, 0.000000000000000000, 0.000000000000000000 ) ) ;
#3532=AXIS2_PLACEMENT_3D ( 'NONE', #3817, #9507, #7046 ) ;
#3537=CIRCLE ( 'NONE', #4894, 6.248999999999999666 ) ;
#3541=CARTESIAN_POINT ( 'NONE',  ( -2.000000000000000000, -0.1221666339523208161, -6.247805719894685694 ) ) ;
#3543=CARTESIAN_POINT ( 'NONE',  ( -2.000000000000000000, 0.000000000000000000, 0.000000000000000000 ) ) ;
#3558=DIRECTION ( 'NONE',  ( -1.000000000000000000, 0.000000000000000000, 0.000000000000000000 ) ) ;
#3567=ORIENTED_EDGE ( 'NONE', *, *, #1681, .T. ) ;
#3570=DIRECTION ( 'NONE',  ( -1.000000000000000000, -0.000000000000000000, -0.000000000000000000 ) ) ;
#3572=DIRECTION ( 'NONE',  ( 0.000000000000000000, -7.228014483236698281E-18, -1.000000000000000000 ) ) ;
#3573=ORIENTED_EDGE ( 'NONE', *, *, #470, .F. ) ;
#3599=CYLINDRICAL_SURFACE ( 'NONE', #657, 6.248999999999999666 ) ;
#3605=CYLINDRICAL_SURFACE ( 'NONE', #4142, 6.248999999999999666 ) ;
#3617=CARTESIAN_POINT ( 'NONE',  ( -10.00000000000000000, 0.000000000000000000, 0.000000000000000000 ) ) ;
#3622=EDGE_CURVE ( 'NONE', #9335, #201, #9238, .T. ) ;
#3630=DIRECTION ( 'NONE',  ( 0.000000000000000000, 0.000000000000000000, -1.000000000000000000 ) ) ;
#3631=CARTESIAN_POINT ( 'NONE',  ( -2.000000000000000000, -2.834406817834849601, -8.013497238472808704 ) ) ;
#3632=VECTOR ( 'NONE', #4768, 1000.000000000000000 ) ;
#3635=EDGE_CURVE ( 'NONE', #2207, #5532, #8442, .T. ) ;
#3642=DIRECTION ( 'NONE',  ( 0.000000000000000000, 0.000000000000000000, 1.000000000000000000 ) ) ;
#3658=EDGE_CURVE ( 'NONE', #2344, #1777, #484, .T. ) ;
#3659=DIRECTION ( 'NONE',  ( -1.000000000000000000, 0.000000000000000000, 0.000000000000000000 ) ) ;
#3670=CARTESIAN_POINT ( 'NONE',  ( 10.00000000000000178, 2.449293598294706414E-16, -2.000000000000000000 ) ) ;
#3671=FACE_OUTER_BOUND ( 'NONE', #5284, .T. ) ;
#3676=EDGE_CURVE ( 'NONE', #2207, #3855, #8409, .T. ) ;
#3677=LINE ( 'NONE', #4520, #7801 ) ;
#3680=ORIENTED_EDGE ( 'NONE', *, *, #3373, .F. ) ;
#3683=CARTESIAN_POINT ( 'NONE',  ( 10.00000000000000000, 4.561279057474473930, -4.271385531633122845 ) ) ;
#3685=CARTESIAN_POINT ( 'NONE',  ( 10.00000000000000000, 0.000000000000000000, 0.000000000000000000 ) ) ;
#3691=CYLINDRICAL_SURFACE ( 'NONE', #5930, 3.000000000000000000 ) ;
#3722=CARTESIAN_POINT ( 'NONE',  ( 0.000000000000000000, -7.063614741696270016, 2.343061888689530026 ) ) ;
#3727=DIRECTION ( 'NONE',  ( 0.000000000000000000, 0.000000000000000000, 1.000000000000000000 ) ) ;
#3741=CARTESIAN_POINT ( 'NONE',  ( 10.00000000000000000, -7.063614741696270016, 2.343061888689530026 ) ) ;
#3742=ORIENTED_EDGE ( 'NONE', *, *, #3826, .T. ) ;
#3744=ORIENTED_EDGE ( 'NONE', *, *, #6863, .F. ) ;
#3747=DIRECTION ( 'NONE',  ( -1.000000000000000000, -0.000000000000000000, -0.000000000000000000 ) ) ;
#3749=ORIENTED_EDGE ( 'NONE', *, *, #4316, .F. ) ;
#3760=FACE_OUTER_BOUND ( 'NONE', #9277, .T. ) ;
#3766=EDGE_CURVE ( 'NONE', #7393, #8683, #1460, .T. ) ;
#3777=EDGE_CURVE ( 'NONE', #7761, #8717, #6535, .T. ) ;
#3778=CARTESIAN_POINT ( 'NONE',  ( 10.00000000000000000, 0.000000000000000000, 0.000000000000000000 ) ) ;
#3785=COLOUR_RGB ( '', 0.09019608, 0.27058824, 0.51372549) ;
#3793=ORIENTED_EDGE ( 'NONE', *, *, #3272, .F. ) ;
#3794=AXIS2_PLACEMENT_3D ( 'NONE', #7256, #6355, #6458 ) ;
#3801=DIRECTION ( 'NONE',  ( 0.000000000000000000, 0.000000000000000000, 1.000000000000000000 ) ) ;
#3810=FACE_OUTER_BOUND ( 'NONE', #9958, .T. ) ;
#3816=AXIS2_PLACEMENT_3D ( 'NONE', #9085, #4994, #5042 ) ;
#3817=CARTESIAN_POINT ( 'NONE',  ( -2.000000000000000000, -6.700937042937042065, -2.183447440113260196 ) ) ;
#3820=AXIS2_PLACEMENT_3D ( 'NONE', #646, #10367, #3630 ) ;
#3826=EDGE_CURVE ( 'NONE', #7785, #9442, #1383, .T. ) ;
#3828=EDGE_CURVE ( 'NONE', #9494, #4339, #4607, .T. ) ;
#3840=DIRECTION ( 'NONE',  ( 0.000000000000000000, 0.000000000000000000, -1.000000000000000000 ) ) ;
#3846=VERTEX_POINT ( 'NONE', #9718 ) ;
#3850=EDGE_CURVE ( 'NONE', #8011, #346, #611, .T. ) ;
#3855=VERTEX_POINT ( 'NONE', #4875 ) ;
#3864=CARTESIAN_POINT ( 'NONE',  ( 10.00000000000000000, 0.000000000000000000, 0.000000000000000000 ) ) ;
#3879=AXIS2_PLACEMENT_3D ( 'NONE', #2224, #5444, #7892 ) ;
#3884=FILL_AREA_STYLE ('',( #5472 ) ) ;
#3896=ORIENTED_EDGE ( 'NONE', *, *, #1681, .F. ) ;
#3903=CARTESIAN_POINT ( 'NONE',  ( 4.000000000000000888, 4.058600654062950674, -7.468451026206158083 ) ) ;
#3908=AXIS2_PLACEMENT_3D ( 'NONE', #1271, #6190, #429 ) ;
#3910=CARTESIAN_POINT ( 'NONE',  ( 8.000000000000001776, -5.233522515400054864, -4.720195129223331065 ) ) ;
#3913=DIRECTION ( 'NONE',  ( 0.000000000000000000, 0.000000000000000000, 1.000000000000000000 ) ) ;
#3914=CARTESIAN_POINT ( 'NONE',  ( -2.000000000000000000, -6.106419733534973915, -3.518755179752866447 ) ) ;
#3917=EDGE_CURVE ( 'NONE', #5731, #6226, #10106, .T. ) ;
#3933=EDGE_LOOP ( 'NONE', ( #9170, #6733, #6814, #3966 ) ) ;
#3948=DIRECTION ( 'NONE',  ( -1.000000000000000000, -0.000000000000000000, -0.000000000000000000 ) ) ;
#3949=EDGE_CURVE ( 'NONE', #201, #6339, #6623, .T. ) ;
#3961=ORIENTED_EDGE ( 'NONE', *, *, #4316, .T. ) ;
#3966=ORIENTED_EDGE ( 'NONE', *, *, #5179, .T. ) ;
#3976=EDGE_CURVE ( 'NONE', #1830, #145, #1650, .T. ) ;
#3994=ORIENTED_EDGE ( 'NONE', *, *, #5376, .T. ) ;
#3995=FACE_OUTER_BOUND ( 'NONE', #8090, .T. ) ;
#4000=FACE_OUTER_BOUND ( 'NONE', #3933, .T. ) ;
#4005=ORIENTED_EDGE ( 'NONE', *, *, #9069, .F. ) ;
#4012=ORIENTED_EDGE ( 'NONE', *, *, #1723, .T. ) ;
#4017=DIRECTION ( 'NONE',  ( 0.000000000000000000, 0.000000000000000000, 1.000000000000000000 ) ) ;
#4027=LINE ( 'NONE', #3076, #1270 ) ;
#4041=FACE_OUTER_BOUND ( 'NONE', #1791, .T. ) ;
#4047=EDGE_CURVE ( 'NONE', #9691, #4320, #8071, .T. ) ;
#4053=CARTESIAN_POINT ( 'NONE',  ( 10.00000000000000000, -6.200809695932781196, 0.7745709230444935978 ) ) ;
#4055=AXIS2_PLACEMENT_3D ( 'NONE', #6666, #219, #3495 ) ;
#4059=VECTOR ( 'NONE', #8888, 1000.000000000000000 ) ;
#4062=ORIENTED_EDGE ( 'NONE', *, *, #8126, .T. ) ;
#4071=CARTESIAN_POINT ( 'NONE',  ( 10.00000000000000000, -0.1221666339523208161, -6.247805719894685694 ) ) ;
#4074=AXIS2_PLACEMENT_3D ( 'NONE', #4953, #8199, #9848 ) ;
#4086=CARTESIAN_POINT ( 'NONE',  ( -2.000000000000000000, 0.000000000000000000, 0.000000000000000000 ) ) ;
#4088=ORIENTED_EDGE ( 'NONE', *, *, #2734, .T. ) ;
#4092=DIRECTION ( 'NONE',  ( 0.000000000000000000, -7.993605777301128669E-15, -1.000000000000000000 ) ) ;
#4098=DIRECTION ( 'NONE',  ( -1.000000000000000000, 0.000000000000000000, 0.000000000000000000 ) ) ;
#4106=ORIENTED_EDGE ( 'NONE', *, *, #4133, .F. ) ;
#4107=ADVANCED_FACE ( 'NONE', ( #7686 ), #10080, .T. ) ;
#4119=ORIENTED_EDGE ( 'NONE', *, *, #2513, .T. ) ;
#4129=DIRECTION ( 'NONE',  ( 0.000000000000000000, 0.000000000000000000, 1.000000000000000000 ) ) ;
#4130=CIRCLE ( 'NONE', #5480, 8.500000000000000000 ) ;
#4133=EDGE_CURVE ( 'NONE', #4614, #5123, #168, .T. ) ;
#4135=ORIENTED_EDGE ( 'NONE', *, *, #10174, .T. ) ;
#4142=AXIS2_PLACEMENT_3D ( 'NONE', #2125, #7797, #1322 ) ;
#4144=FACE_OUTER_BOUND ( 'NONE', #7522, .T. ) ;
#4150=CIRCLE ( 'NONE', #2974, 3.000000000000000000 ) ;
#4152=EDGE_CURVE ( 'NONE', #7510, #4614, #8620, .T. ) ;
#4156=VERTEX_POINT ( 'NONE', #7574 ) ;
#4163=ORIENTED_EDGE ( 'NONE', *, *, #4922, .T. ) ;
#4184=ORIENTED_EDGE ( 'NONE', *, *, #8126, .F. ) ;
#4210=CIRCLE ( 'NONE', #3532, 3.000000000000000444 ) ;
#4213=ORIENTED_EDGE ( 'NONE', *, *, #4717, .T. ) ;
#4220=ADVANCED_FACE ( 'NONE', ( #8482 ), #1215, .F. ) ;
#4223=ADVANCED_FACE ( 'NONE', ( #5291 ), #4492, .T. ) ;
#4228=AXIS2_PLACEMENT_3D ( 'NONE', #3910, #5442, #7136 ) ;
#4229=ORIENTED_EDGE ( 'NONE', *, *, #4640, .T. ) ;
#4232=ORIENTED_EDGE ( 'NONE', *, *, #9554, .T. ) ;
#4238=VERTEX_POINT ( 'NONE', #10234 ) ;
#4240=CIRCLE ( 'NONE', #3908, 6.248999999999999666 ) ;
#4244=DIRECTION ( 'NONE',  ( 0.000000000000000000, 0.000000000000000000, 1.000000000000000000 ) ) ;
#4256=FACE_OUTER_BOUND ( 'NONE', #1056, .T. ) ;
#4260=ORIENTED_EDGE ( 'NONE', *, *, #9091, .F. ) ;
#4263=ORIENTED_EDGE ( 'NONE', *, *, #6696, .T. ) ;
#4265=EDGE_CURVE ( 'NONE', #467, #5853, #6071, .T. ) ;
#4266=EDGE_LOOP ( 'NONE', ( #4433, #6896, #8282, #1953 ) ) ;
#4276=AXIS2_PLACEMENT_3D ( 'NONE', #3914, #7140, #3118 ) ;
#4281=FACE_OUTER_BOUND ( 'NONE', #8776, .T. ) ;
#4283=VERTEX_POINT ( 'NONE', #9598 ) ;
#4296=DIRECTION ( 'NONE',  ( -1.000000000000000000, 0.000000000000000000, -0.000000000000000000 ) ) ;
#4316=EDGE_CURVE ( 'NONE', #6690, #2207, #8298, .T. ) ;
#4320=VERTEX_POINT ( 'NONE', #8790 ) ;
#4325=VECTOR ( 'NONE', #10295, 1000.000000000000000 ) ;
#4333=CARTESIAN_POINT ( 'NONE',  ( 10.00000000000000000, 5.241389472434725860, -4.711457988287000909 ) ) ;
#4339=VERTEX_POINT ( 'NONE', #626 ) ;
#4341=ADVANCED_FACE ( 'NONE', ( #7139 ), #5341, .T. ) ;
#4343=CARTESIAN_POINT ( 'NONE',  ( 10.00000000000000000, -6.200809695932771426, -0.7745709230445765314 ) ) ;
#4346=DIRECTION ( 'NONE',  ( 0.000000000000000000, 0.000000000000000000, 1.000000000000000000 ) ) ;
#4354=ORIENTED_EDGE ( 'NONE', *, *, #2403, .T. ) ;
#4357=DIRECTION ( 'NONE',  ( -1.000000000000000000, -0.000000000000000000, -0.000000000000000000 ) ) ;
#4359=EDGE_CURVE ( 'NONE', #9494, #467, #1864, .T. ) ;
#4371=AXIS2_PLACEMENT_3D ( 'NONE', #9395, #6943, #8697 ) ;
#4379=ORIENTED_EDGE ( 'NONE', *, *, #213, .T. ) ;
#4380=DIRECTION ( 'NONE',  ( -1.000000000000000000, 0.000000000000000000, 0.000000000000000000 ) ) ;
#4386=CARTESIAN_POINT ( 'NONE',  ( -2.000000000000000000, 0.000000000000000000, 0.000000000000000000 ) ) ;
#4389=ORIENTED_EDGE ( 'NONE', *, *, #5130, .F. ) ;
#4392=AXIS2_PLACEMENT_3D ( 'NONE', #9853, #1629, #6385 ) ;
#4396=AXIS2_PLACEMENT_3D ( 'NONE', #3219, #4758, #732 ) ;
#4401=DIRECTION ( 'NONE',  ( -1.000000000000000000, -0.000000000000000000, -0.000000000000000000 ) ) ;
#4406=AXIS2_PLACEMENT_3D ( 'NONE', #963, #7637, #3450 ) ;
#4408=EDGE_CURVE ( 'NONE', #9974, #6869, #7605, .T. ) ;
#4411=VECTOR ( 'NONE', #8883, 1000.000000000000000 ) ;
#4412=DIRECTION ( 'NONE',  ( 0.000000000000000000, 0.000000000000000000, 1.000000000000000000 ) ) ;
#4422=VERTEX_POINT ( 'NONE', #6279 ) ;
#4423=CARTESIAN_POINT ( 'NONE',  ( 0.000000000000000000, -7.063614741696270016, 8.843061888689529582 ) ) ;
#4433=ORIENTED_EDGE ( 'NONE', *, *, #1957, .T. ) ;
#4438=CARTESIAN_POINT ( 'NONE',  ( 4.000000000000000888, -7.673322273190750664, 3.656518192455050276 ) ) ;
#4445=CYLINDRICAL_SURFACE ( 'NONE', #2431, 3.000000000000000000 ) ;
#4448=CARTESIAN_POINT ( 'NONE',  ( -2.000000000000000000, 7.003298780661491918, -4.817032923780498521 ) ) ;
#4452=DIRECTION ( 'NONE',  ( 0.000000000000000000, 0.000000000000000000, 1.000000000000000000 ) ) ;
#4461=DIRECTION ( 'NONE',  ( 0.000000000000000000, -0.000000000000000000, 1.000000000000000000 ) ) ;
#4464=EDGE_LOOP ( 'NONE', ( #6695, #9053, #5028, #4263 ) ) ;
#4468=EDGE_CURVE ( 'NONE', #4238, #1944, #723, .T. ) ;
#4469=EDGE_CURVE ( 'NONE', #10319, #4238, #2900, .T. ) ;
#4478=ORIENTED_EDGE ( 'NONE', *, *, #8174, .F. ) ;
#4486=AXIS2_PLACEMENT_3D ( 'NONE', #254, #7303, #3481 ) ;
#4490=CARTESIAN_POINT ( 'NONE',  ( -2.000000000000000000, 5.793104693147763662, 2.343061888689530026 ) ) ;
#4491=VERTEX_POINT ( 'NONE', #826 ) ;
#4492=CYLINDRICAL_SURFACE ( 'NONE', #7951, 6.248999999999999666 ) ;
#4497=EDGE_CURVE ( 'NONE', #4339, #5618, #9487, .T. ) ;
#4503=DIRECTION ( 'NONE',  ( -1.000000000000000000, -0.000000000000000000, -0.000000000000000000 ) ) ;
#4512=CARTESIAN_POINT ( 'NONE',  ( 10.00000000000000000, 0.000000000000000000, 0.000000000000000000 ) ) ;
#4518=ORIENTED_EDGE ( 'NONE', *, *, #5300, .F. ) ;
#4520=CARTESIAN_POINT ( 'NONE',  ( 4.000000000000000888, -7.673322273190701814, -3.656518192455153748 ) ) ;
#4532=DIRECTION ( 'NONE',  ( 1.000000000000000000, 0.000000000000000000, 0.000000000000000000 ) ) ;
#4535=EDGE_CURVE ( 'NONE', #8939, #7393, #8153, .T. ) ;
#4543=ORIENTED_EDGE ( 'NONE', *, *, #9279, .T. ) ;
#4544=LINE ( 'NONE', #477, #7803 ) ;
#4545=VECTOR ( 'NONE', #8, 1000.000000000000000 ) ;
#4546=FACE_BOUND ( 'NONE', #2951, .T. ) ;
#4547=DIRECTION ( 'NONE',  ( 1.000000000000000000, 0.000000000000000000, 0.000000000000000000 ) ) ;
#4549=EDGE_CURVE ( 'NONE', #8074, #5539, #8808, .T. ) ;
#4552=DIRECTION ( 'NONE',  ( -1.000000000000000000, -0.000000000000000000, 0.000000000000000000 ) ) ;
#4562=CIRCLE ( 'NONE', #11, 8.500000000000000000 ) ;
#4589=ORIENTED_EDGE ( 'NONE', *, *, #328, .F. ) ;
#4598=LINE ( 'NONE', #7898, #3229 ) ;
#4601=DIRECTION ( 'NONE',  ( 0.000000000000000000, 0.000000000000000000, 1.000000000000000000 ) ) ;
#4602=DIRECTION ( 'NONE',  ( 1.000000000000000000, 0.000000000000000000, 0.000000000000000000 ) ) ;
#4607=LINE ( 'NONE', #7849, #9771 ) ;
#4614=VERTEX_POINT ( 'NONE', #8097 ) ;
#4615=CIRCLE ( 'NONE', #6990, 8.500000000000000000 ) ;
#4619=DIRECTION ( 'NONE',  ( 1.000000000000000000, -0.000000000000000000, 0.000000000000000000 ) ) ;
#4630=CARTESIAN_POINT ( 'NONE',  ( -10.00000000000000000, 0.000000000000000000, 0.000000000000000000 ) ) ;
#4640=EDGE_CURVE ( 'NONE', #3105, #6166, #8935, .T. ) ;
#4651=VECTOR ( 'NONE', #4380, 1000.000000000000000 ) ;
#4653=DIRECTION ( 'NONE',  ( -1.000000000000000000, -0.000000000000000000, 0.000000000000000000 ) ) ;
#4654=DIRECTION ( 'NONE',  ( -1.000000000000000000, -0.000000000000000000, -0.000000000000000000 ) ) ;
#4659=AXIS2_PLACEMENT_3D ( 'NONE', #869, #9886, #8242 ) ;
#4663=AXIS2_PLACEMENT_3D ( 'NONE', #6991, #1382, #9503 ) ;
#4665=CARTESIAN_POINT ( 'NONE',  ( 8.000000000000001776, 0.005878491403557128264, -7.047692205288322853 ) ) ;
#4678=CARTESIAN_POINT ( 'NONE',  ( 10.00000000000000000, 1.106368468154538931, -8.427689411260562480 ) ) ;
#4685=CARTESIAN_POINT ( 'NONE',  ( -2.000000000000000000, 1.418488851014483076, -6.085876303339363247 ) ) ;
#4704=ORIENTED_EDGE ( 'NONE', *, *, #5130, .T. ) ;
#4713=AXIS2_PLACEMENT_3D ( 'NONE', #3081, #6091, #2025 ) ;
#4716=DIRECTION ( 'NONE',  ( 0.000000000000000000, 0.000000000000000000, 1.000000000000000000 ) ) ;
#4717=EDGE_CURVE ( 'NONE', #5181, #837, #2375, .T. ) ;
#4728=DIRECTION ( 'NONE',  ( -1.000000000000000000, -0.000000000000000000, 0.000000000000000000 ) ) ;
#4737=ORIENTED_EDGE ( 'NONE', *, *, #3034, .T. ) ;
#4750=AXIS2_PLACEMENT_3D ( 'NONE', #10218, #7723, #2102 ) ;
#4751=EDGE_CURVE ( 'NONE', #216, #1449, #7453, .T. ) ;
#4758=DIRECTION ( 'NONE',  ( 1.000000000000000000, 0.000000000000000000, 0.000000000000000000 ) ) ;
#4759=AXIS2_PLACEMENT_3D ( 'NONE', #773, #612, #3840 ) ;
#4760=EDGE_LOOP ( 'NONE', ( #9513, #5036, #3961, #8318 ) ) ;
#4761=DIRECTION ( 'NONE',  ( -1.000000000000000000, -0.000000000000000000, -0.000000000000000000 ) ) ;
#4768=DIRECTION ( 'NONE',  ( -1.000000000000000000, 0.000000000000000000, 0.000000000000000000 ) ) ;
#4777=EDGE_CURVE ( 'NONE', #1449, #6865, #3677, .T. ) ;
#4780=ORIENTED_EDGE ( 'NONE', *, *, #253, .F. ) ;
#4783=CARTESIAN_POINT ( 'NONE',  ( 4.000000000000000888, -8.497168642645966941, 0.2193742428684610779 ) ) ;
#4785=ORIENTED_EDGE ( 'NONE', *, *, #3034, .F. ) ;
#4791=DIRECTION ( 'NONE',  ( 0.000000000000000000, 0.000000000000000000, 1.000000000000000000 ) ) ;
#4796=EDGE_LOOP ( 'NONE', ( #8780, #8050, #1233, #250 ) ) ;
#4799=CYLINDRICAL_SURFACE ( 'NONE', #5586, 8.500000000000000000 ) ;
#4809=EDGE_LOOP ( 'NONE', ( #5547, #718, #6124, #7469 ) ) ;
#4825=DIRECTION ( 'NONE',  ( 0.000000000000000000, 0.000000000000000000, -1.000000000000000000 ) ) ;
#4835=CARTESIAN_POINT ( 'NONE',  ( -2.000000000000000000, -7.673322273190701814, -3.656518192455153748 ) ) ;
#4841=CARTESIAN_POINT ( 'NONE',  ( 10.00000000000000000, 0.000000000000000000, 0.000000000000000000 ) ) ;
#4842=AXIS2_PLACEMENT_3D ( 'NONE', #1489, #10354, #7152 ) ;
#4853=VERTEX_POINT ( 'NONE', #4678 ) ;
#4861=VERTEX_POINT ( 'NONE', #10263 ) ;
#4865=ORIENTED_EDGE ( 'NONE', *, *, #2733, .F. ) ;
#4869=EDGE_CURVE ( 'NONE', #6398, #1737, #2713, .T. ) ;
#4875=CARTESIAN_POINT ( 'NONE',  ( 10.00000000000000000, 4.438567988583180579, -7.249076783337634389 ) ) ;
#4883=FACE_OUTER_BOUND ( 'NONE', #9299, .T. ) ;
#4891=CARTESIAN_POINT ( 'NONE',  ( -2.000000000000001776, 0.000000000000000000, 0.000000000000000000 ) ) ;
#4894=AXIS2_PLACEMENT_3D ( 'NONE', #3778, #2993, #3727 ) ;
#4913=VECTOR ( 'NONE', #4728, 1000.000000000000000 ) ;
#4922=EDGE_CURVE ( 'NONE', #6226, #5731, #1024, .T. ) ;
#4928=DIRECTION ( 'NONE',  ( -1.000000000000000000, -0.000000000000000000, 0.000000000000000000 ) ) ;
#4929=AXIS2_PLACEMENT_3D ( 'NONE', #5969, #4098, #2410 ) ;
#4930=DIRECTION ( 'NONE',  ( 0.000000000000000000, 1.421085471520200372E-14, -1.000000000000000000 ) ) ;
#4934=EDGE_CURVE ( 'NONE', #5853, #9996, #4562, .T. ) ;
#4941=DIRECTION ( 'NONE',  ( -1.000000000000000000, -0.000000000000000000, -0.000000000000000000 ) ) ;
#4944=VERTEX_POINT ( 'NONE', #2413 ) ;
#4951=ORIENTED_EDGE ( 'NONE', *, *, #2007, .F. ) ;
#4953=CARTESIAN_POINT ( 'NONE',  ( 10.00000000000000000, -5.233522515400054864, -4.720195129223331065 ) ) ;
#4960=PLANE ( 'NONE',  #10228 ) ;
#4971=ORIENTED_EDGE ( 'NONE', *, *, #5102, .F. ) ;
#4973=VECTOR ( 'NONE', #2762, 1000.000000000000000 ) ;
#4974=ORIENTED_EDGE ( 'NONE', *, *, #8446, .F. ) ;
#4975=CARTESIAN_POINT ( 'NONE',  ( 8.000000000000001776, 7.008469740302802897, 0.7425307242148025955 ) ) ;
#4976=EDGE_CURVE ( 'NONE', #3364, #8683, #5630, .T. ) ;
#4984=ORIENTED_EDGE ( 'NONE', *, *, #3777, .T. ) ;
#4991=AXIS2_PLACEMENT_3D ( 'NONE', #8377, #8275, #1001 ) ;
#4992=ADVANCED_FACE ( 'NONE', ( #4000 ), #765, .T. ) ;
#4993=FACE_OUTER_BOUND ( 'NONE', #5049, .T. ) ;
#4994=DIRECTION ( 'NONE',  ( 0.000000000000000000, -7.228014483236699822E-18, -1.000000000000000000 ) ) ;
#4996=EDGE_CURVE ( 'NONE', #8513, #897, #6605, .T. ) ;
#4999=DIRECTION ( 'NONE',  ( 0.000000000000000000, 0.000000000000000000, 1.000000000000000000 ) ) ;
#5010=ORIENTED_EDGE ( 'NONE', *, *, #6094, .T. ) ;
#5022=EDGE_LOOP ( 'NONE', ( #1626, #727, #3315, #2657 ) ) ;
#5028=ORIENTED_EDGE ( 'NONE', *, *, #3949, .F. ) ;
#5030=CARTESIAN_POINT ( 'NONE',  ( 8.000000000000001776, -6.700937042937042065, 0.8165525598867396928 ) ) ;
#5032=EDGE_LOOP ( 'NONE', ( #42, #848, #3166, #4379 ) ) ;
#5036=ORIENTED_EDGE ( 'NONE', *, *, #5429, .F. ) ;
#5042=DIRECTION ( 'NONE',  ( 0.000000000000000000, 1.000000000000000000, -7.228014483236699822E-18 ) ) ;
#5049=EDGE_LOOP ( 'NONE', ( #7137, #1513, #8756, #9433 ) ) ;
#5051=FACE_OUTER_BOUND ( 'NONE', #5817, .T. ) ;
#5056=VERTEX_POINT ( 'NONE', #10352 ) ;
#5063=ORIENTED_EDGE ( 'NONE', *, *, #8869, .F. ) ;
#5064=CARTESIAN_POINT ( 'NONE',  ( 8.000000000000001776, 1.418488851014483076, -6.085876303339363247 ) ) ;
#5077=ORIENTED_EDGE ( 'NONE', *, *, #9315, .F. ) ;
#5085=ORIENTED_EDGE ( 'NONE', *, *, #1646, .T. ) ;
#5089=VECTOR ( 'NONE', #903, 1000.000000000000000 ) ;
#5093=AXIS2_PLACEMENT_3D ( 'NONE', #464, #4532, #6014 ) ;
#5096=AXIS2_PLACEMENT_3D ( 'NONE', #1184, #5206, #4412 ) ;
#5097=CARTESIAN_POINT ( 'NONE',  ( -2.000000000000000000, 0.000000000000000000, 0.000000000000000000 ) ) ;
#5102=EDGE_CURVE ( 'NONE', #1286, #4614, #6357, .T. ) ;
#5108=CYLINDRICAL_SURFACE ( 'NONE', #1545, 8.500000000000000000 ) ;
#5117=EDGE_CURVE ( 'NONE', #5532, #8167, #686, .T. ) ;
#5123=VERTEX_POINT ( 'NONE', #6938 ) ;
#5126=FILL_AREA_STYLE ('',( #214 ) ) ;
#5129=CYLINDRICAL_SURFACE ( 'NONE', #4991, 3.000000000000000000 ) ;
#5130=EDGE_CURVE ( 'NONE', #5902, #8074, #7748, .T. ) ;
#5141=CARTESIAN_POINT ( 'NONE',  ( 10.00000000000000178, 0.000000000000000000, 2.000000000000000000 ) ) ;
#5179=EDGE_CURVE ( 'NONE', #7785, #4320, #7970, .T. ) ;
#5180=( LENGTH_UNIT ( ) NAMED_UNIT ( * ) SI_UNIT ( .MILLI., .METRE. ) );
#5181=VERTEX_POINT ( 'NONE', #9458 ) ;
#5182=CARTESIAN_POINT ( 'NONE',  ( 8.000000000000001776, -6.200809695932781196, 0.7745709230444935978 ) ) ;
#5186=CARTESIAN_POINT ( 'NONE',  ( 4.000000000000000888, 4.438567988583180579, -7.249076783337634389 ) ) ;
#5206=DIRECTION ( 'NONE',  ( -1.000000000000000000, -0.000000000000000000, -0.000000000000000000 ) ) ;
#5217=DIRECTION ( 'NONE',  ( 0.000000000000000000, 0.000000000000000000, -1.000000000000000000 ) ) ;
#5219=DIRECTION ( 'NONE',  ( -1.000000000000000000, -0.000000000000000000, -0.000000000000000000 ) ) ;
#5234=AXIS2_PLACEMENT_3D ( 'NONE', #9119, #10132, #2067 ) ;
#5237=CARTESIAN_POINT ( 'NONE',  ( -2.000000000000000000, -4.147285340411748678, -5.698247474649444477 ) ) ;
#5248=CARTESIAN_POINT ( 'NONE',  ( 10.00000000000000178, 0.000000000000000000, 0.000000000000000000 ) ) ;
#5249=AXIS2_PLACEMENT_3D ( 'NONE', #408, #5219, #7771 ) ;
#5266=ADVANCED_FACE ( 'NONE', ( #392 ), #1392, .T. ) ;
#5267=DIRECTION ( 'NONE',  ( 0.000000000000000000, 1.000000000000000000, 0.000000000000000000 ) ) ;
#5269=DIRECTION ( 'NONE',  ( -1.000000000000000000, -0.000000000000000000, -0.000000000000000000 ) ) ;
#5277=LINE ( 'NONE', #4423, #8068 ) ;
#5279=CARTESIAN_POINT ( 'NONE',  ( 10.00000000000000000, 2.429606751577122026, -5.757344182232885466 ) ) ;
#5280=EDGE_LOOP ( 'NONE', ( #352, #2623, #5290, #950 ) ) ;
#5284=EDGE_LOOP ( 'NONE', ( #3470, #891, #9547, #6343 ) ) ;
#5290=ORIENTED_EDGE ( 'NONE', *, *, #9802, .T. ) ;
#5291=FACE_OUTER_BOUND ( 'NONE', #8376, .T. ) ;
#5296=CARTESIAN_POINT ( 'NONE',  ( -2.000000000000000000, 6.226349476952025341, -0.5315761383463619705 ) ) ;
#5300=EDGE_CURVE ( 'NONE', #7393, #2426, #8316, .T. ) ;
#5311=EDGE_CURVE ( 'NONE', #8939, #3364, #17, .T. ) ;
#5312=ORIENTED_EDGE ( 'NONE', *, *, #5772, .F. ) ;
#5323=( GEOMETRIC_REPRESENTATION_CONTEXT ( 3 ) GLOBAL_UNCERTAINTY_ASSIGNED_CONTEXT ( ( #9267 ) ) GLOBAL_UNIT_ASSIGNED_CONTEXT ( ( #5180, #7681, #8427 ) ) REPRESENTATION_CONTEXT ( 'NONE', 'WORKASPACE' ) );
#5341=CYLINDRICAL_SURFACE ( 'NONE', #838, 6.248999999999999666 ) ;
#5342=CIRCLE ( 'NONE', #3820, 3.000000000000000000 ) ;
#5362=DIRECTION ( 'NONE',  ( 0.000000000000000000, 0.000000000000000000, 1.000000000000000000 ) ) ;
#5363=DIRECTION ( 'NONE',  ( 0.000000000000000000, 0.000000000000000000, 1.000000000000000000 ) ) ;
#5376=EDGE_CURVE ( 'NONE', #216, #7456, #6368, .T. ) ;
#5395=FACE_OUTER_BOUND ( 'NONE', #1941, .T. ) ;
#5396=CARTESIAN_POINT ( 'NONE',  ( -2.000000000000000000, 0.000000000000000000, 0.000000000000000000 ) ) ;
#5398=CARTESIAN_POINT ( 'NONE',  ( -2.000000000000000000, 3.771202944355774189, -4.982773259188334691 ) ) ;
#5399=CARTESIAN_POINT ( 'NONE',  ( -2.000000000000000000, 1.459547570502460978, -6.894905428400257996 ) ) ;
#5409=FACE_OUTER_BOUND ( 'NONE', #5499, .T. ) ;
#5411=AXIS2_PLACEMENT_3D ( 'NONE', #3864, #9392, #9502 ) ;
#5422=VECTOR ( 'NONE', #1659, 1000.000000000000000 ) ;
#5424=AXIS2_PLACEMENT_3D ( 'NONE', #1758, #7266, #8178 ) ;
#5429=EDGE_CURVE ( 'NONE', #6690, #4861, #6415, .T. ) ;
#5442=DIRECTION ( 'NONE',  ( -1.000000000000000000, -0.000000000000000000, 0.000000000000000000 ) ) ;
#5444=DIRECTION ( 'NONE',  ( -1.000000000000000000, -0.000000000000000000, -0.000000000000000000 ) ) ;
#5447=EDGE_LOOP ( 'NONE', ( #630, #10288, #1318, #4163 ) ) ;
#5449=DIRECTION ( 'NONE',  ( -1.000000000000000000, -0.000000000000000000, -0.000000000000000000 ) ) ;
#5454=FACE_OUTER_BOUND ( 'NONE', #10279, .T. ) ;
#5462=ADVANCED_FACE ( 'NONE', ( #4883 ), #2506, .T. ) ;
#5463=DIRECTION ( 'NONE',  ( -1.000000000000000000, -0.000000000000000000, 0.000000000000000000 ) ) ;
#5465=CIRCLE ( 'NONE', #238, 3.000000000000000444 ) ;
#5471=VERTEX_POINT ( 'NONE', #6308 ) ;
#5472=FILL_AREA_STYLE_COLOUR ( '', #1172 ) ;
#5473=DIRECTION ( 'NONE',  ( -1.000000000000000000, -0.000000000000000000, -0.000000000000000000 ) ) ;
#5478=ORIENTED_EDGE ( 'NONE', *, *, #4996, .T. ) ;
#5479=EDGE_CURVE ( 'NONE', #2644, #897, #7223, .T. ) ;
#5480=AXIS2_PLACEMENT_3D ( 'NONE', #10140, #2920, #9388 ) ;
#5482=ORIENTED_EDGE ( 'NONE', *, *, #9476, .F. ) ;
#5495=ORIENTED_EDGE ( 'NONE', *, *, #7262, .F. ) ;
#5499=EDGE_LOOP ( 'NONE', ( #1522, #3742, #8028, #2170 ) ) ;
#5514=ADVANCED_FACE ( 'NONE', ( #3810 ), #3605, .T. ) ;
#5518=AXIS2_PLACEMENT_3D ( 'NONE', #8119, #6461, #3393 ) ;
#5523=ORIENTED_EDGE ( 'NONE', *, *, #5311, .F. ) ;
#5528=( NAMED_UNIT ( * ) PLANE_ANGLE_UNIT ( ) SI_UNIT ( $, .RADIAN. ) );
#5529=DIRECTION ( 'NONE',  ( 0.000000000000000000, 0.000000000000000000, 1.000000000000000000 ) ) ;
#5532=VERTEX_POINT ( 'NONE', #5398 ) ;
#5539=VERTEX_POINT ( 'NONE', #7042 ) ;
#5547=ORIENTED_EDGE ( 'NONE', *, *, #3766, .F. ) ;
#5548=DIRECTION ( 'NONE',  ( -1.000000000000000000, -0.000000000000000000, -0.000000000000000000 ) ) ;
#5556=LINE ( 'NONE', #9715, #3632 ) ;
#5561=CARTESIAN_POINT ( 'NONE',  ( 10.00000000000000000, 6.704570150427012543, -2.172265885002586661 ) ) ;
#5571=ORIENTED_EDGE ( 'NONE', *, *, #6696, .F. ) ;
#5575=DIRECTION ( 'NONE',  ( 0.000000000000000000, 0.000000000000000000, -1.000000000000000000 ) ) ;
#5583=EDGE_CURVE ( 'NONE', #2046, #10267, #10428, .T. ) ;
#5584=ORIENTED_EDGE ( 'NONE', *, *, #1348, .F. ) ;
#5586=AXIS2_PLACEMENT_3D ( 'NONE', #4630, #7124, #661 ) ;
#5591=VECTOR ( 'NONE', #3019, 1000.000000000000000 ) ;
#5601=AXIS2_PLACEMENT_3D ( 'NONE', #1237, #2089, #5362 ) ;
#5606=CARTESIAN_POINT ( 'NONE',  ( -2.000000000000000000, 0.000000000000000000, 0.000000000000000000 ) ) ;
#5610=DIRECTION ( 'NONE',  ( 0.000000000000000000, 0.000000000000000000, 1.000000000000000000 ) ) ;
#5616=CARTESIAN_POINT ( 'NONE',  ( 4.000000000000000888, 8.357095590591340439, 1.552080310331536372 ) ) ;
#5618=VERTEX_POINT ( 'NONE', #1224 ) ;
#5625=VERTEX_POINT ( 'NONE', #4448 ) ;
#5628=CYLINDRICAL_SURFACE ( 'NONE', #9827, 3.000000000000000000 ) ;
#5630=LINE ( 'NONE', #7335, #4913 ) ;
#5638=AXIS2_PLACEMENT_3D ( 'NONE', #8919, #8234, #4092 ) ;
#5648=( GEOMETRIC_REPRESENTATION_CONTEXT ( 3 ) GLOBAL_UNCERTAINTY_ASSIGNED_CONTEXT ( ( #1209 ) ) GLOBAL_UNIT_ASSIGNED_CONTEXT ( ( #6662, #9010, #5862 ) ) REPRESENTATION_CONTEXT ( 'NONE', 'WORKASPACE' ) );
#5651=CARTESIAN_POINT ( 'NONE',  ( -2.000000000000000000, 52.93638525830372998, 8.843061888689529582 ) ) ;
#5662=CARTESIAN_POINT ( 'NONE',  ( 4.000000000000000888, 6.745408891279613961, -5.171987904998036178 ) ) ;
#5672=SHAPE_DEFINITION_REPRESENTATION ( #8765, #8347 ) ;
#5687=EDGE_CURVE ( 'NONE', #8580, #8403, #4027, .T. ) ;
#5689=ORIENTED_EDGE ( 'NONE', *, *, #9219, .F. ) ;
#5692=ORIENTED_EDGE ( 'NONE', *, *, #3272, .T. ) ;
#5703=ORIENTED_EDGE ( 'NONE', *, *, #4535, .T. ) ;
#5711=DIRECTION ( 'NONE',  ( -1.000000000000000000, -0.000000000000000000, -0.000000000000000000 ) ) ;
#5715=ORIENTED_EDGE ( 'NONE', *, *, #2265, .T. ) ;
#5720=CARTESIAN_POINT ( 'NONE',  ( 8.000000000000001776, 6.704570150427012543, -2.172265885002586661 ) ) ;
#5731=VERTEX_POINT ( 'NONE', #1485 ) ;
#5733=VECTOR ( 'NONE', #905, 1000.000000000000000 ) ;
#5734=ORIENTED_EDGE ( 'NONE', *, *, #8760, .T. ) ;
#5737=DIRECTION ( 'NONE',  ( 0.000000000000000000, 0.000000000000000000, 1.000000000000000000 ) ) ;
#5739=VERTEX_POINT ( 'NONE', #3128 ) ;
#5744=VECTOR ( 'NONE', #9478, 1000.000000000000000 ) ;
#5747=ADVANCED_FACE ( 'NONE', ( #5454 ), #1429, .T. ) ;
#5748=ORIENTED_EDGE ( 'NONE', *, *, #9343, .T. ) ;
#5764=DIRECTION ( 'NONE',  ( 0.000000000000000000, 0.000000000000000000, 1.000000000000000000 ) ) ;
#5772=EDGE_CURVE ( 'NONE', #371, #6398, #5556, .T. ) ;
#5778=DIRECTION ( 'NONE',  ( 0.000000000000000000, 0.000000000000000000, 1.000000000000000000 ) ) ;
#5780=DIRECTION ( 'NONE',  ( 0.000000000000000000, 0.000000000000000000, 1.000000000000000000 ) ) ;
#5802=DIRECTION ( 'NONE',  ( -1.000000000000000000, 0.000000000000000000, -0.000000000000000000 ) ) ;
#5804=ORIENTED_EDGE ( 'NONE', *, *, #6685, .F. ) ;
#5812=ORIENTED_EDGE ( 'NONE', *, *, #4934, .F. ) ;
#5817=EDGE_LOOP ( 'NONE', ( #402, #7399, #10364, #4543 ) ) ;
#5827=CARTESIAN_POINT ( 'NONE',  ( 10.00000000000000178, 0.000000000000000000, 0.000000000000000000 ) ) ;
#5829=DIRECTION ( 'NONE',  ( -1.000000000000000000, 0.000000000000000000, -0.000000000000000000 ) ) ;
#5830=ADVANCED_FACE ( 'NONE', ( #4281 ), #6713, .T. ) ;
#5833=DIRECTION ( 'NONE',  ( 0.000000000000000000, 0.000000000000000000, 1.000000000000000000 ) ) ;
#5841=ADVANCED_FACE ( 'NONE', ( #3389 ), #2546, .T. ) ;
#5847=DIRECTION ( 'NONE',  ( -1.000000000000000000, -0.000000000000000000, -0.000000000000000000 ) ) ;
#5853=VERTEX_POINT ( 'NONE', #2649 ) ;
#5862=( NAMED_UNIT ( * ) SI_UNIT ( $, .STERADIAN. ) SOLID_ANGLE_UNIT ( ) );
#5875=CARTESIAN_POINT ( 'NONE',  ( 10.00000000000000000, 0.000000000000000000, 0.000000000000000000 ) ) ;
#5878=DIRECTION ( 'NONE',  ( 0.000000000000000000, 0.000000000000000000, 1.000000000000000000 ) ) ;
#5889=FACE_OUTER_BOUND ( 'NONE', #1136, .T. ) ;
#5892=CARTESIAN_POINT ( 'NONE',  ( 10.00000000000000000, 0.000000000000000000, 0.000000000000000000 ) ) ;
#5902=VERTEX_POINT ( 'NONE', #1854 ) ;
#5913=CIRCLE ( 'NONE', #8805, 3.000000000000000000 ) ;
#5930=AXIS2_PLACEMENT_3D ( 'NONE', #9266, #1307, #3642 ) ;
#5932=CARTESIAN_POINT ( 'NONE',  ( 10.00000000000000000, 1.459547570502460978, -6.894905428400257996 ) ) ;
#5942=CARTESIAN_POINT ( 'NONE',  ( 10.00000000000000000, 0.000000000000000000, 0.000000000000000000 ) ) ;
#5967=ADVANCED_FACE ( 'NONE', ( #6563 ), #5129, .T. ) ;
#5969=CARTESIAN_POINT ( 'NONE',  ( 8.000000000000001776, -7.009698679648292519, 0.7308381473896652381 ) ) ;
#5974=CYLINDRICAL_SURFACE ( 'NONE', #4406, 3.000000000000000000 ) ;
#5977=VECTOR ( 'NONE', #10041, 1000.000000000000000 ) ;
#5979=DIRECTION ( 'NONE',  ( -1.000000000000000000, 0.000000000000000000, -0.000000000000000000 ) ) ;
#5984=AXIS2_PLACEMENT_3D ( 'NONE', #1018, #4296, #285 ) ;
#5989=EDGE_LOOP ( 'NONE', ( #2691, #304, #5571, #2054 ) ) ;
#5991=DIRECTION ( 'NONE',  ( 0.000000000000000000, 0.000000000000000000, -1.000000000000000000 ) ) ;
#5993=EDGE_LOOP ( 'NONE', ( #8998, #4389, #4737, #5085 ) ) ;
#6014=DIRECTION ( 'NONE',  ( 0.000000000000000000, 0.000000000000000000, -1.000000000000000000 ) ) ;
#6015=AXIS2_PLACEMENT_3D ( 'NONE', #3288, #2449, #2603 ) ;
#6027=CARTESIAN_POINT ( 'NONE',  ( -2.000000000000000000, 0.000000000000000000, 0.000000000000000000 ) ) ;
#6033=CARTESIAN_POINT ( 'NONE',  ( 8.000000000000001776, 3.771202944355774189, -4.982773259188334691 ) ) ;
#6042=FACE_OUTER_BOUND ( 'NONE', #5989, .T. ) ;
#6045=ORIENTED_EDGE ( 'NONE', *, *, #3498, .F. ) ;
#6047=DIRECTION ( 'NONE',  ( -1.000000000000000000, -0.000000000000000000, 0.000000000000000000 ) ) ;
#6063=CARTESIAN_POINT ( 'NONE',  ( -2.000000000000000000, 5.904264776415100613, 2.046865518294722630 ) ) ;
#6067=SURFACE_STYLE_USAGE ( .BOTH. , #2907 ) ;
#6071=CIRCLE ( 'NONE', #8459, 3.000000000000000000 ) ;
#6073=ORIENTED_EDGE ( 'NONE', *, *, #5117, .T. ) ;
#6074=CARTESIAN_POINT ( 'NONE',  ( 8.000000000000001776, -1.471047635026825784, -6.892461014225975013 ) ) ;
#6075=CIRCLE ( 'NONE', #672, 3.000000000000000000 ) ;
#6079=ORIENTED_EDGE ( 'NONE', *, *, #671, .T. ) ;
#6087=VECTOR ( 'NONE', #10064, 1000.000000000000000 ) ;
#6091=DIRECTION ( 'NONE',  ( -1.000000000000000000, -0.000000000000000000, 0.000000000000000000 ) ) ;
#6094=EDGE_CURVE ( 'NONE', #8717, #9974, #1154, .T. ) ;
#6100=AXIS2_PLACEMENT_3D ( 'NONE', #2263, #2317, #669 ) ;
#6106=FACE_OUTER_BOUND ( 'NONE', #607, .T. ) ;
#6108=EDGE_CURVE ( 'NONE', #10253, #8513, #4150, .T. ) ;
#6115=LINE ( 'NONE', #218, #25 ) ;
#6116=CARTESIAN_POINT ( 'NONE',  ( -2.000000000000000000, -5.979767908488829775, -1.814490771706245065 ) ) ;
#6122=CARTESIAN_POINT ( 'NONE',  ( 10.00000000000000000, -5.522688772756355391, -6.461416928141300531 ) ) ;
#6124=ORIENTED_EDGE ( 'NONE', *, *, #5311, .T. ) ;
#6138=LINE ( 'NONE', #8491, #4973 ) ;
#6140=EDGE_CURVE ( 'NONE', #8424, #9096, #2850, .T. ) ;
#6166=VERTEX_POINT ( 'NONE', #8581 ) ;
#6179=AXIS2_PLACEMENT_3D ( 'NONE', #6899, #9297, #5363 ) ;
#6186=CARTESIAN_POINT ( 'NONE',  ( 10.00000000000000000, -6.700937042937042065, 0.8165525598867396928 ) ) ;
#6190=DIRECTION ( 'NONE',  ( -1.000000000000000000, -0.000000000000000000, -0.000000000000000000 ) ) ;
#6208=CARTESIAN_POINT ( 'NONE',  ( -2.000000000000000000, -3.573533178329545645, -5.126388750707257635 ) ) ;
#6210=CARTESIAN_POINT ( 'NONE',  ( -2.000000000000000000, 0.000000000000000000, 0.000000000000000000 ) ) ;
#6220=CARTESIAN_POINT ( 'NONE',  ( 10.00000000000000000, -7.063614741696270016, 8.843061888689529582 ) ) ;
#6226=VERTEX_POINT ( 'NONE', #2374 ) ;
#6231=ORIENTED_EDGE ( 'NONE', *, *, #6108, .T. ) ;
#6243=DIRECTION ( 'NONE',  ( -1.000000000000000000, -0.000000000000000000, 0.000000000000000000 ) ) ;
#6254=CIRCLE ( 'NONE', #7457, 3.000000000000000000 ) ;
#6258=PLANE ( 'NONE',  #6951 ) ;
#6269=ORIENTED_EDGE ( 'NONE', *, *, #4468, .F. ) ;
#6279=CARTESIAN_POINT ( 'NONE',  ( 10.00000000000000000, -7.851777359433979697, -3.255701506262516087 ) ) ;
#6281=DIRECTION ( 'NONE',  ( -1.000000000000000000, -0.000000000000000000, -0.000000000000000000 ) ) ;
#6287=FACE_OUTER_BOUND ( 'NONE', #3367, .T. ) ;
#6288=EDGE_LOOP ( 'NONE', ( #2329, #5689, #10449, #1249 ) ) ;
#6289=DIRECTION ( 'NONE',  ( 0.000000000000000000, -1.734723475976807094E-15, -1.000000000000000000 ) ) ;
#6299=CARTESIAN_POINT ( 'NONE',  ( 4.000000000000000888, -7.851777359434023218, 3.255701506262409506 ) ) ;
#6301=LINE ( 'NONE', #8648, #6729 ) ;
#6305=FACE_OUTER_BOUND ( 'NONE', #3326, .T. ) ;
#6308=CARTESIAN_POINT ( 'NONE',  ( -2.000000000000000000, 6.745408891279613961, -5.171987904998036178 ) ) ;
#6312=FACE_OUTER_BOUND ( 'NONE', #9774, .T. ) ;
#6313=ORIENTED_EDGE ( 'NONE', *, *, #470, .T. ) ;
#6315=DIRECTION ( 'NONE',  ( -1.000000000000000000, -0.000000000000000000, -0.000000000000000000 ) ) ;
#6320=ORIENTED_EDGE ( 'NONE', *, *, #2718, .T. ) ;
#6321=ADVANCED_FACE ( 'NONE', ( #569 ), #7191, .T. ) ;
#6327=ORIENTED_EDGE ( 'NONE', *, *, #4751, .T. ) ;
#6339=VERTEX_POINT ( 'NONE', #5651 ) ;
#6343=ORIENTED_EDGE ( 'NONE', *, *, #4934, .T. ) ;
#6350=EDGE_CURVE ( 'NONE', #346, #8266, #7356, .T. ) ;
#6353=DIRECTION ( 'NONE',  ( 0.000000000000000000, 1.421085471520200372E-14, -1.000000000000000000 ) ) ;
#6355=DIRECTION ( 'NONE',  ( -1.000000000000000000, 0.000000000000000000, 0.000000000000000000 ) ) ;
#6356=AXIS2_PLACEMENT_3D ( 'NONE', #9028, #1764, #1922 ) ;
#6357=LINE ( 'NONE', #2283, #2554 ) ;
#6359=DIRECTION ( 'NONE',  ( -1.000000000000000000, 0.000000000000000000, 0.000000000000000000 ) ) ;
#6368=LINE ( 'NONE', #71, #5422 ) ;
#6373=CARTESIAN_POINT ( 'NONE',  ( 8.000000000000001776, 0.000000000000000000, 0.000000000000000000 ) ) ;
#6382=DIRECTION ( 'NONE',  ( -1.000000000000000000, -0.000000000000000000, -0.000000000000000000 ) ) ;
#6385=DIRECTION ( 'NONE',  ( 0.000000000000000000, 0.000000000000000000, -1.000000000000000000 ) ) ;
#6398=VERTEX_POINT ( 'NONE', #2484 ) ;
#6402=CARTESIAN_POINT ( 'NONE',  ( 0.000000000000000000, 52.93638525830372998, 8.843061888689529582 ) ) ;
#6415=LINE ( 'NONE', #645, #8712 ) ;
#6423=CARTESIAN_POINT ( 'NONE',  ( 10.00000000000000000, -4.147285340411748678, -5.698247474649444477 ) ) ;
#6424=DIRECTION ( 'NONE',  ( -1.000000000000000000, -0.000000000000000000, -0.000000000000000000 ) ) ;
#6433=LINE ( 'NONE', #9696, #4411 ) ;
#6434=CIRCLE ( 'NONE', #5249, 3.000000000000000000 ) ;
#6446=AXIS2_PLACEMENT_3D ( 'NONE', #1581, #6281, #9537 ) ;
#6452=DIRECTION ( 'NONE',  ( 0.000000000000000000, 0.000000000000000000, 1.000000000000000000 ) ) ;
#6458=DIRECTION ( 'NONE',  ( 0.000000000000000000, 0.000000000000000000, 1.000000000000000000 ) ) ;
#6461=DIRECTION ( 'NONE',  ( -1.000000000000000000, -0.000000000000000000, -0.000000000000000000 ) ) ;
#6484=ORIENTED_EDGE ( 'NONE', *, *, #10127, .T. ) ;
#6487=FACE_OUTER_BOUND ( 'NONE', #6288, .T. ) ;
#6496=CYLINDRICAL_SURFACE ( 'NONE', #4486, 6.248999999999999666 ) ;
#6498=ORIENTED_EDGE ( 'NONE', *, *, #7065, .T. ) ;
#6501=DIRECTION ( 'NONE',  ( -1.000000000000000000, -0.000000000000000000, -0.000000000000000000 ) ) ;
#6507=AXIS2_PLACEMENT_3D ( 'NONE', #5720, #10366, #7108 ) ;
#6521=AXIS2_PLACEMENT_3D ( 'NONE', #305, #1998, #5217 ) ;
#6524=DIRECTION ( 'NONE',  ( -1.000000000000000000, 0.000000000000000000, -0.000000000000000000 ) ) ;
#6532=ADVANCED_FACE ( 'NONE', ( #9001 ), #6496, .T. ) ;
#6535=CIRCLE ( 'NONE', #4842, 3.000000000000000000 ) ;
#6541=DIRECTION ( 'NONE',  ( 0.000000000000000000, 0.000000000000000000, 1.000000000000000000 ) ) ;
#6542=ORIENTED_EDGE ( 'NONE', *, *, #926, .T. ) ;
#6563=FACE_OUTER_BOUND ( 'NONE', #5032, .T. ) ;
#6564=LINE ( 'NONE', #5662, #3402 ) ;
#6575=CYLINDRICAL_SURFACE ( 'NONE', #6356, 3.000000000000000000 ) ;
#6583=DIRECTION ( 'NONE',  ( 0.000000000000000000, 0.000000000000000000, -1.000000000000000000 ) ) ;
#6585=AXIS2_PLACEMENT_3D ( 'NONE', #5237, #8335, #422 ) ;
#6590=DIRECTION ( 'NONE',  ( -1.000000000000000000, 0.000000000000000000, -0.000000000000000000 ) ) ;
#6605=CIRCLE ( 'NONE', #7624, 8.500000000000000000 ) ;
#6606=ORIENTED_EDGE ( 'NONE', *, *, #3373, .T. ) ;
#6609=CIRCLE ( 'NONE', #4759, 3.000000000000000888 ) ;
#6623=LINE ( 'NONE', #1005, #2139 ) ;
#6662=( LENGTH_UNIT ( ) NAMED_UNIT ( * ) SI_UNIT ( .MILLI., .METRE. ) );
#6666=CARTESIAN_POINT ( 'NONE',  ( -2.000000000000000000, -5.233522515400119701, 4.720195129223260899 ) ) ;
#6685=EDGE_CURVE ( 'NONE', #6166, #1958, #601, .T. ) ;
#6690=VERTEX_POINT ( 'NONE', #3683 ) ;
#6693=VECTOR ( 'NONE', #9832, 1000.000000000000000 ) ;
#6695=ORIENTED_EDGE ( 'NONE', *, *, #4468, .T. ) ;
#6696=EDGE_CURVE ( 'NONE', #201, #4238, #5277, .T. ) ;
#6713=CYLINDRICAL_SURFACE ( 'NONE', #3471, 3.000000000000000000 ) ;
#6714=ORIENTED_EDGE ( 'NONE', *, *, #1809, .F. ) ;
#6725=CARTESIAN_POINT ( 'NONE',  ( 8.000000000000001776, 5.904264776415100613, 2.046865518294722630 ) ) ;
#6729=VECTOR ( 'NONE', #2180, 1000.000000000000000 ) ;
#6732=EDGE_CURVE ( 'NONE', #2162, #9974, #5342, .T. ) ;
#6733=ORIENTED_EDGE ( 'NONE', *, *, #10068, .F. ) ;
#6734=EDGE_CURVE ( 'NONE', #8580, #7607, #8366, .T. ) ;
#6739=CARTESIAN_POINT ( 'NONE',  ( -2.000000000000000000, 5.241389472434725860, -4.711457988287000909 ) ) ;
#6744=AXIS2_PLACEMENT_3D ( 'NONE', #28, #3304, #972 ) ;
#6748=ORIENTED_EDGE ( 'NONE', *, *, #227, .T. ) ;
#6750=CIRCLE ( 'NONE', #3042, 3.000000000000000000 ) ;
#6770=AXIS2_PLACEMENT_3D ( 'NONE', #1290, #4357, #9196 ) ;
#6781=CARTESIAN_POINT ( 'NONE',  ( 4.000000000000000888, -5.848742439617878652, -6.167836887841048110 ) ) ;
#6784=CIRCLE ( 'NONE', #6100, 8.500000000000000000 ) ;
#6785=DIRECTION ( 'NONE',  ( 0.000000000000000000, 0.000000000000000000, 1.000000000000000000 ) ) ;
#6794=ORIENTED_EDGE ( 'NONE', *, *, #1723, .F. ) ;
#6797=CARTESIAN_POINT ( 'NONE',  ( 10.00000000000000000, 5.793104693147763662, 2.343061888689530026 ) ) ;
#6814=ORIENTED_EDGE ( 'NONE', *, *, #3826, .F. ) ;
#6824=CYLINDRICAL_SURFACE ( 'NONE', #4929, 3.000000000000000000 ) ;
#6827=CIRCLE ( 'NONE', #6833, 6.248999999999999666 ) ;
#6833=AXIS2_PLACEMENT_3D ( 'NONE', #9605, #7041, #6353 ) ;
#6844=ORIENTED_EDGE ( 'NONE', *, *, #3766, .T. ) ;
#6845=DIRECTION ( 'NONE',  ( 0.000000000000000000, 0.000000000000000000, 1.000000000000000000 ) ) ;
#6850=ORIENTED_EDGE ( 'NONE', *, *, #10362, .F. ) ;
#6863=EDGE_CURVE ( 'NONE', #1777, #2162, #1632, .T. ) ;
#6865=VERTEX_POINT ( 'NONE', #4835 ) ;
#6869=VERTEX_POINT ( 'NONE', #915 ) ;
#6873=DIRECTION ( 'NONE',  ( -1.000000000000000000, 0.000000000000000000, 0.000000000000000000 ) ) ;
#6883=CARTESIAN_POINT ( 'NONE',  ( -2.000000000000000000, 0.6700234925293845345, -8.473551116235670477 ) ) ;
#6889=DIRECTION ( 'NONE',  ( -1.000000000000000000, 0.000000000000000000, 0.000000000000000000 ) ) ;
#6896=ORIENTED_EDGE ( 'NONE', *, *, #7475, .T. ) ;
#6899=CARTESIAN_POINT ( 'NONE',  ( 10.00000000000000000, 0.000000000000000000, 0.000000000000000000 ) ) ;
#6910=CARTESIAN_POINT ( 'NONE',  ( 4.000000000000000888, 7.003298780661491918, -4.817032923780498521 ) ) ;
#6916=FACE_OUTER_BOUND ( 'NONE', #1751, .T. ) ;
#6918=ADVANCED_FACE ( 'NONE', ( #4041 ), #6575, .T. ) ;
#6928=ORIENTED_EDGE ( 'NONE', *, *, #4469, .F. ) ;
#6930=DIRECTION ( 'NONE',  ( 1.000000000000000000, 0.000000000000000000, 0.000000000000000000 ) ) ;
#6931=ADVANCED_FACE ( 'NONE', ( #4993 ), #3408, .T. ) ;
#6937=CIRCLE ( 'NONE', #4396, 3.000000000000000000 ) ;
#6938=CARTESIAN_POINT ( 'NONE',  ( -2.000000000000000000, -2.417132211460011337, -8.149077976821821778 ) ) ;
#6943=DIRECTION ( 'NONE',  ( -1.000000000000000000, -0.000000000000000000, -0.000000000000000000 ) ) ;
#6951=AXIS2_PLACEMENT_3D ( 'NONE', #3722, #5267, #4461 ) ;
#6957=CARTESIAN_POINT ( 'NONE',  ( -2.000000000000000000, -1.471047635026825784, -6.892461014225975013 ) ) ;
#6963=ORIENTED_EDGE ( 'NONE', *, *, #2986, .T. ) ;
#6971=ORIENTED_EDGE ( 'NONE', *, *, #6732, .T. ) ;
#6974=ADVANCED_FACE ( 'NONE', ( #8288 ), #7490, .T. ) ;
#6980=CARTESIAN_POINT ( 'NONE',  ( 10.00000000000000000, 0.000000000000000000, 0.000000000000000000 ) ) ;
#6981=EDGE_CURVE ( 'NONE', #8011, #7252, #8393, .T. ) ;
#6986=AXIS2_PLACEMENT_3D ( 'NONE', #7144, #5449, #8638 ) ;
#6988=DIRECTION ( 'NONE',  ( 0.000000000000000000, 0.000000000000000000, 1.000000000000000000 ) ) ;
#6990=AXIS2_PLACEMENT_3D ( 'NONE', #8144, #7439, #2622 ) ;
#6991=CARTESIAN_POINT ( 'NONE',  ( 10.00000000000000000, -6.700937042937042065, -2.183447440113260196 ) ) ;
#7001=CARTESIAN_POINT ( 'NONE',  ( -2.000000000000000000, 0.005878491403557128264, -7.047692205288322853 ) ) ;
#7002=EDGE_CURVE ( 'NONE', #6339, #7874, #1015, .T. ) ;
#7008=SURFACE_SIDE_STYLE ('',( #7116 ) ) ;
#7016=AXIS2_PLACEMENT_3D ( 'NONE', #5248, #582, #380 ) ;
#7017=CARTESIAN_POINT ( 'NONE',  ( -2.000000000000000000, 6.100541242131515496, -3.528937025535514138 ) ) ;
#7025=VERTEX_POINT ( 'NONE', #2563 ) ;
#7027=AXIS2_PLACEMENT_3D ( 'NONE', #1336, #3570, #10154 ) ;
#7035=ADVANCED_FACE ( 'NONE', ( #3506 ), #2614, .T. ) ;
#7038=VECTOR ( 'NONE', #1170, 1000.000000000000000 ) ;
#7039=CARTESIAN_POINT ( 'NONE',  ( -2.000000000000000000, -6.700937042937042065, 0.8165525598867396928 ) ) ;
#7041=DIRECTION ( 'NONE',  ( -1.000000000000000000, -0.000000000000000000, -0.000000000000000000 ) ) ;
#7042=CARTESIAN_POINT ( 'NONE',  ( -2.000000000000000000, -6.200809695932771426, -0.7745709230445765314 ) ) ;
#7046=DIRECTION ( 'NONE',  ( 0.000000000000000000, 0.000000000000000000, -1.000000000000000000 ) ) ;
#7065=EDGE_CURVE ( 'NONE', #7761, #2162, #483, .T. ) ;
#7068=CARTESIAN_POINT ( 'NONE',  ( -2.000000000000000000, 0.000000000000000000, 0.000000000000000000 ) ) ;
#7075=DIRECTION ( 'NONE',  ( 1.000000000000000000, -0.000000000000000000, 0.000000000000000000 ) ) ;
#7078=ORIENTED_EDGE ( 'NONE', *, *, #9315, .T. ) ;
#7084=CARTESIAN_POINT ( 'NONE',  ( 10.00000000000000000, 4.137773741518453008, -5.705158055754754542 ) ) ;
#7087=ORIENTED_EDGE ( 'NONE', *, *, #9219, .T. ) ;
#7090=CARTESIAN_POINT ( 'NONE',  ( 0.000000000000000000, 0.000000000000000000, 0.000000000000000000 ) ) ;
#7099=CARTESIAN_POINT ( 'NONE',  ( 10.00000000000000000, 5.471841788314748989, -3.018103451449677621 ) ) ;
#7108=DIRECTION ( 'NONE',  ( 0.000000000000000000, 0.000000000000000000, 1.000000000000000000 ) ) ;
#7116=SURFACE_STYLE_FILL_AREA ( #3884 ) ;
#7122=CIRCLE ( 'NONE', #691, 8.500000000000000000 ) ;
#7124=DIRECTION ( 'NONE',  ( -1.000000000000000000, -0.000000000000000000, -0.000000000000000000 ) ) ;
#7131=ORIENTED_EDGE ( 'NONE', *, *, #8550, .F. ) ;
#7132=LINE ( 'NONE', #3903, #10026 ) ;
#7136=DIRECTION ( 'NONE',  ( 0.000000000000000000, 0.000000000000000000, 1.000000000000000000 ) ) ;
#7137=ORIENTED_EDGE ( 'NONE', *, *, #2428, .F. ) ;
#7139=FACE_OUTER_BOUND ( 'NONE', #5993, .T. ) ;
#7140=DIRECTION ( 'NONE',  ( -1.000000000000000000, -0.000000000000000000, -0.000000000000000000 ) ) ;
#7144=CARTESIAN_POINT ( 'NONE',  ( -2.000000000000000000, -7.009698679648282749, -0.7308381473897593850 ) ) ;
#7151=ADVANCED_FACE ( 'NONE', ( #3760 ), #8695, .F. ) ;
#7152=DIRECTION ( 'NONE',  ( 0.000000000000000000, 0.000000000000000000, 1.000000000000000000 ) ) ;
#7160=CIRCLE ( 'NONE', #5638, 8.500000000000000000 ) ;
#7164=VERTEX_POINT ( 'NONE', #1431 ) ;
#7175=ORIENTED_EDGE ( 'NONE', *, *, #10362, .T. ) ;
#7191=CYLINDRICAL_SURFACE ( 'NONE', #7545, 6.248999999999999666 ) ;
#7205=EDGE_CURVE ( 'NONE', #897, #9050, #111, .T. ) ;
#7206=ORIENTED_EDGE ( 'NONE', *, *, #5117, .F. ) ;
#7221=ORIENTED_EDGE ( 'NONE', *, *, #3850, .T. ) ;
#7223=LINE ( 'NONE', #4783, #2121 ) ;
#7224=CARTESIAN_POINT ( 'NONE',  ( -2.000000000000000000, 7.008469740302810891, -0.7425307242147085596 ) ) ;
#7230=CARTESIAN_POINT ( 'NONE',  ( -10.00000000000000000, 0.000000000000000000, 0.000000000000000000 ) ) ;
#7234=ORIENTED_EDGE ( 'NONE', *, *, #2801, .F. ) ;
#7238=ORIENTED_EDGE ( 'NONE', *, *, #3676, .T. ) ;
#7252=VERTEX_POINT ( 'NONE', #9609 ) ;
#7256=CARTESIAN_POINT ( 'NONE',  ( 8.000000000000001776, 6.100541242131515496, -3.528937025535514138 ) ) ;
#7262=EDGE_CURVE ( 'NONE', #2426, #5739, #801, .T. ) ;
#7264=EDGE_CURVE ( 'NONE', #9050, #8424, #3323, .T. ) ;
#7265=CIRCLE ( 'NONE', #2866, 6.248999999999999666 ) ;
#7266=DIRECTION ( 'NONE',  ( -1.000000000000000000, -0.000000000000000000, -0.000000000000000000 ) ) ;
#7269=AXIS2_PLACEMENT_3D ( 'NONE', #177, #4401, #5833 ) ;
#7277=CARTESIAN_POINT ( 'NONE',  ( -2.000000000000000000, -5.522688772756355391, -6.461416928141300531 ) ) ;
#7289=FACE_OUTER_BOUND ( 'NONE', #10277, .T. ) ;
#7295=ORIENTED_EDGE ( 'NONE', *, *, #4359, .T. ) ;
#7298=VECTOR ( 'NONE', #3197, 1000.000000000000000 ) ;
#7301=ORIENTED_EDGE ( 'NONE', *, *, #2986, .F. ) ;
#7303=DIRECTION ( 'NONE',  ( -1.000000000000000000, 0.000000000000000000, -0.000000000000000000 ) ) ;
#7304=CARTESIAN_POINT ( 'NONE',  ( 10.00000000000000000, 0.6700234925293845345, -8.473551116235670477 ) ) ;
#7305=CIRCLE ( 'NONE', #1376, 8.500000000000000000 ) ;
#7314=ORIENTED_EDGE ( 'NONE', *, *, #2007, .T. ) ;
#7325=DIRECTION ( 'NONE',  ( 1.000000000000000000, 0.000000000000000000, 0.000000000000000000 ) ) ;
#7335=CARTESIAN_POINT ( 'NONE',  ( 8.000000000000001776, -3.573533178329545645, -5.126388750707257635 ) ) ;
#7343=LINE ( 'NONE', #2472, #9171 ) ;
#7345=CARTESIAN_POINT ( 'NONE',  ( 10.00000000000000000, 52.93638525830372998, 2.343061888689529582 ) ) ;
#7356=LINE ( 'NONE', #5064, #942 ) ;
#7363=ORIENTED_EDGE ( 'NONE', *, *, #3498, .T. ) ;
#7369=CARTESIAN_POINT ( 'NONE',  ( -2.000000000000000000, -5.349675154362301122, -3.229702268444983648 ) ) ;
#7378=AXIS2_PLACEMENT_3D ( 'NONE', #174, #5829, #5878 ) ;
#7380=CIRCLE ( 'NONE', #2812, 3.000000000000000000 ) ;
#7383=CARTESIAN_POINT ( 'NONE',  ( 10.00000000000000000, -2.652816298622379776, -5.657964889053610946 ) ) ;
#7393=VERTEX_POINT ( 'NONE', #695 ) ;
#7399=ORIENTED_EDGE ( 'NONE', *, *, #2734, .F. ) ;
#7433=DIRECTION ( 'NONE',  ( 0.000000000000000000, 0.000000000000000000, 1.000000000000000000 ) ) ;
#7435=DIRECTION ( 'NONE',  ( -1.000000000000000000, -0.000000000000000000, -0.000000000000000000 ) ) ;
#7438=EDGE_CURVE ( 'NONE', #7164, #9442, #2373, .T. ) ;
#7439=DIRECTION ( 'NONE',  ( -1.000000000000000000, -0.000000000000000000, -0.000000000000000000 ) ) ;
#7452=ORIENTED_EDGE ( 'NONE', *, *, #7264, .F. ) ;
#7453=CIRCLE ( 'NONE', #8133, 3.000000000000000000 ) ;
#7456=VERTEX_POINT ( 'NONE', #7369 ) ;
#7457=AXIS2_PLACEMENT_3D ( 'NONE', #7017, #1405, #9637 ) ;
#7458=ORIENTED_EDGE ( 'NONE', *, *, #3125, .F. ) ;
#7469=ORIENTED_EDGE ( 'NONE', *, *, #4976, .T. ) ;
#7475=EDGE_CURVE ( 'NONE', #10281, #8011, #8303, .T. ) ;
#7490=CYLINDRICAL_SURFACE ( 'NONE', #10097, 6.248999999999999666 ) ;
#7500=CARTESIAN_POINT ( 'NONE',  ( 8.000000000000001776, 4.137773741518453008, -5.705158055754754542 ) ) ;
#7510=VERTEX_POINT ( 'NONE', #3541 ) ;
#7522=EDGE_LOOP ( 'NONE', ( #7891, #3567, #4229, #1180 ) ) ;
#7524=DIRECTION ( 'NONE',  ( -1.000000000000000000, -0.000000000000000000, -0.000000000000000000 ) ) ;
#7545=AXIS2_PLACEMENT_3D ( 'NONE', #3064, #8055, #4017 ) ;
#7558=CARTESIAN_POINT ( 'NONE',  ( -2.000000000000000000, -7.673322273190750664, 3.656518192455050276 ) ) ;
#7574=CARTESIAN_POINT ( 'NONE',  ( 10.00000000000000000, -5.848742439617878652, -6.167836887841048110 ) ) ;
#7598=CARTESIAN_POINT ( 'NONE',  ( 10.00000000000000000, -4.724769925181144359, -4.089810527897808079 ) ) ;
#7600=ORIENTED_EDGE ( 'NONE', *, *, #1047, .T. ) ;
#7602=DIRECTION ( 'NONE',  ( 0.000000000000000000, 0.000000000000000000, 1.000000000000000000 ) ) ;
#7605=CIRCLE ( 'NONE', #2028, 8.500000000000000000 ) ;
#7607=VERTEX_POINT ( 'NONE', #4490 ) ;
#7624=AXIS2_PLACEMENT_3D ( 'NONE', #4841, #1507, #7980 ) ;
#7632=DIRECTION ( 'NONE',  ( -1.000000000000000000, -0.000000000000000000, -0.000000000000000000 ) ) ;
#7637=DIRECTION ( 'NONE',  ( -1.000000000000000000, 0.000000000000000000, 0.000000000000000000 ) ) ;
#7681=( NAMED_UNIT ( * ) PLANE_ANGLE_UNIT ( ) SI_UNIT ( $, .RADIAN. ) );
#7686=FACE_OUTER_BOUND ( 'NONE', #4796, .T. ) ;
#7696=CIRCLE ( 'NONE', #6986, 3.000000000000000000 ) ;
#7700=CARTESIAN_POINT ( 'NONE',  ( 10.00000000000000000, 0.005878491403557128264, -7.047692205288322853 ) ) ;
#7707=DIRECTION ( 'NONE',  ( -1.000000000000000000, -0.000000000000000000, -0.000000000000000000 ) ) ;
#7723=DIRECTION ( 'NONE',  ( -1.000000000000000000, -0.000000000000000000, 0.000000000000000000 ) ) ;
#7742=LINE ( 'NONE', #9386, #5591 ) ;
#7744=FACE_OUTER_BOUND ( 'NONE', #8847, .T. ) ;
#7748=LINE ( 'NONE', #482, #8637 ) ;
#7749=CARTESIAN_POINT ( 'NONE',  ( 8.000000000000001776, 7.008469740302810891, 2.257469275785291440 ) ) ;
#7761=VERTEX_POINT ( 'NONE', #8057 ) ;
#7768=EDGE_CURVE ( 'NONE', #346, #4853, #5913, .T. ) ;
#7769=ORIENTED_EDGE ( 'NONE', *, *, #8869, .T. ) ;
#7771=DIRECTION ( 'NONE',  ( 0.000000000000000000, 0.000000000000000000, 1.000000000000000000 ) ) ;
#7774=AXIS2_PLACEMENT_3D ( 'NONE', #7700, #1227, #4452 ) ;
#7785=VERTEX_POINT ( 'NONE', #2221 ) ;
#7791=CARTESIAN_POINT ( 'NONE',  ( 10.00000000000000000, -2.861184399890952079, -6.440778198864142823 ) ) ;
#7793=CARTESIAN_POINT ( 'NONE',  ( 10.00000000000000000, 5.904264776415129923, -2.046865518294644914 ) ) ;
#7797=DIRECTION ( 'NONE',  ( -1.000000000000000000, 0.000000000000000000, 0.000000000000000000 ) ) ;
#7798=CIRCLE ( 'NONE', #347, 6.248999999999999666 ) ;
#7801=VECTOR ( 'NONE', #2197, 1000.000000000000000 ) ;
#7803=VECTOR ( 'NONE', #6930, 1000.000000000000000 ) ;
#7810=ADVANCED_FACE ( 'NONE', ( #6287 ), #8001, .T. ) ;
#7815=CIRCLE ( 'NONE', #3410, 8.500000000000000000 ) ;
#7817=LINE ( 'NONE', #709, #9245 ) ;
#7826=DIRECTION ( 'NONE',  ( -1.000000000000000000, 0.000000000000000000, 0.000000000000000000 ) ) ;
#7849=CARTESIAN_POINT ( 'NONE',  ( 8.000000000000001776, 5.904264776415129923, -2.046865518294644914 ) ) ;
#7852=EDGE_CURVE ( 'NONE', #9335, #9691, #6937, .T. ) ;
#7862=DIRECTION ( 'NONE',  ( 0.000000000000000000, 0.000000000000000000, 1.000000000000000000 ) ) ;
#7865=ORIENTED_EDGE ( 'NONE', *, *, #7852, .F. ) ;
#7874=VERTEX_POINT ( 'NONE', #836 ) ;
#7881=CARTESIAN_POINT ( 'NONE',  ( -2.000000000000000000, 7.008469740302802897, 0.7425307242148025955 ) ) ;
#7886=VERTEX_POINT ( 'NONE', #7304 ) ;
#7891=ORIENTED_EDGE ( 'NONE', *, *, #10343, .T. ) ;
#7892=DIRECTION ( 'NONE',  ( 0.000000000000000000, 0.000000000000000000, 1.000000000000000000 ) ) ;
#7893=VECTOR ( 'NONE', #9717, 1000.000000000000000 ) ;
#7894=CARTESIAN_POINT ( 'NONE',  ( -2.000000000000000000, 0.000000000000000000, 0.000000000000000000 ) ) ;
#7898=CARTESIAN_POINT ( 'NONE',  ( 4.000000000000000888, 0.6700234925293845345, -8.473551116235670477 ) ) ;
#7900=CYLINDRICAL_SURFACE ( 'NONE', #2941, 6.248999999999999666 ) ;
#7930=ORIENTED_EDGE ( 'NONE', *, *, #5583, .F. ) ;
#7932=FACE_OUTER_BOUND ( 'NONE', #9426, .T. ) ;
#7943=DIRECTION ( 'NONE',  ( 0.000000000000000000, 0.000000000000000000, 1.000000000000000000 ) ) ;
#7950=FACE_BOUND ( 'NONE', #2901, .T. ) ;
#7951=AXIS2_PLACEMENT_3D ( 'NONE', #3015, #2117, #7943 ) ;
#7970=CIRCLE ( 'NONE', #5411, 8.500000000000000000 ) ;
#7975=CARTESIAN_POINT ( 'NONE',  ( 8.000000000000001776, -7.063614741696270016, 3.730353617970412206 ) ) ;
#7977=DIRECTION ( 'NONE',  ( 1.000000000000000000, 0.000000000000000000, 0.000000000000000000 ) ) ;
#7980=DIRECTION ( 'NONE',  ( 0.000000000000000000, 0.000000000000000000, 1.000000000000000000 ) ) ;
#7986=VECTOR ( 'NONE', #882, 1000.000000000000000 ) ;
#7996=CARTESIAN_POINT ( 'NONE',  ( 8.000000000000001776, -0.1221666339523208161, -6.247805719894685694 ) ) ;
#8001=CYLINDRICAL_SURFACE ( 'NONE', #4228, 3.000000000000000000 ) ;
#8006=VERTEX_POINT ( 'NONE', #2895 ) ;
#8011=VERTEX_POINT ( 'NONE', #5279 ) ;
#8028=ORIENTED_EDGE ( 'NONE', *, *, #7438, .F. ) ;
#8030=DIRECTION ( 'NONE',  ( 0.000000000000000000, 0.000000000000000000, 1.000000000000000000 ) ) ;
#8042=CIRCLE ( 'NONE', #1585, 6.248999999999999666 ) ;
#8043=DIRECTION ( 'NONE',  ( 0.000000000000000000, 0.000000000000000000, -1.000000000000000000 ) ) ;
#8050=ORIENTED_EDGE ( 'NONE', *, *, #8613, .F. ) ;
#8055=DIRECTION ( 'NONE',  ( -1.000000000000000000, 0.000000000000000000, -0.000000000000000000 ) ) ;
#8057=CARTESIAN_POINT ( 'NONE',  ( 10.00000000000000000, 7.008469740302810891, 2.257469275785291440 ) ) ;
#8060=DIRECTION ( 'NONE',  ( 0.000000000000000000, 0.000000000000000000, -1.000000000000000000 ) ) ;
#8064=AXIS2_PLACEMENT_3D ( 'NONE', #1562, #2409, #7862 ) ;
#8066=EDGE_CURVE ( 'NONE', #10267, #6226, #9368, .T. ) ;
#8068=VECTOR ( 'NONE', #455, 1000.000000000000000 ) ;
#8071=LINE ( 'NONE', #4438, #2696 ) ;
#8072=CARTESIAN_POINT ( 'NONE',  ( 50.00005079999999680, 2.449293598294706414E-16, -2.000000000000000000 ) ) ;
#8074=VERTEX_POINT ( 'NONE', #6116 ) ;
#8077=DIRECTION ( 'NONE',  ( 0.000000000000000000, 0.000000000000000000, 1.000000000000000000 ) ) ;
#8084=FACE_OUTER_BOUND ( 'NONE', #5280, .T. ) ;
#8090=EDGE_LOOP ( 'NONE', ( #9216, #508, #6850, #5478 ) ) ;
#8097=CARTESIAN_POINT ( 'NONE',  ( -2.000000000000000000, -1.179494851233864106, -6.136676046192498291 ) ) ;
#8117=DIRECTION ( 'NONE',  ( 1.000000000000000000, -0.000000000000000000, 0.000000000000000000 ) ) ;
#8119=CARTESIAN_POINT ( 'NONE',  ( -2.000000000000001776, 0.000000000000000000, 0.000000000000000000 ) ) ;
#8122=ORIENTED_EDGE ( 'NONE', *, *, #9791, .T. ) ;
#8126=EDGE_CURVE ( 'NONE', #5056, #5181, #6434, .T. ) ;
#8133=AXIS2_PLACEMENT_3D ( 'NONE', #3473, #6315, #1342 ) ;
#8139=DIRECTION ( 'NONE',  ( -1.000000000000000000, -0.000000000000000000, -0.000000000000000000 ) ) ;
#8144=CARTESIAN_POINT ( 'NONE',  ( 10.00000000000000000, 0.000000000000000000, 0.000000000000000000 ) ) ;
#8147=CARTESIAN_POINT ( 'NONE',  ( 10.00000000000000000, 52.93638525830372998, 8.843061888689529582 ) ) ;
#8149=DIRECTION ( 'NONE',  ( -1.000000000000000000, -0.000000000000000000, -0.000000000000000000 ) ) ;
#8153=LINE ( 'NONE', #10441, #4059 ) ;
#8160=VECTOR ( 'NONE', #2369, 1000.000000000000000 ) ;
#8167=VERTEX_POINT ( 'NONE', #458 ) ;
#8174=EDGE_CURVE ( 'NONE', #9192, #1286, #7798, .T. ) ;
#8178=DIRECTION ( 'NONE',  ( 0.000000000000000000, 0.000000000000000000, 1.000000000000000000 ) ) ;
#8197=ADVANCED_FACE ( 'NONE', ( #2364 ), #4799, .T. ) ;
#8199=DIRECTION ( 'NONE',  ( -1.000000000000000000, -0.000000000000000000, -0.000000000000000000 ) ) ;
#8208=AXIS2_PLACEMENT_3D ( 'NONE', #8900, #6501, #6452 ) ;
#8234=DIRECTION ( 'NONE',  ( -1.000000000000000000, -0.000000000000000000, -0.000000000000000000 ) ) ;
#8236=EDGE_CURVE ( 'NONE', #1737, #7025, #6254, .T. ) ;
#8240=CARTESIAN_POINT ( 'NONE',  ( 8.000000000000001776, -6.700937042937042065, -2.183447440113260196 ) ) ;
#8242=DIRECTION ( 'NONE',  ( 0.000000000000000000, 0.000000000000000000, -1.000000000000000000 ) ) ;
#8253=CYLINDRICAL_SURFACE ( 'NONE', #6770, 8.500000000000000000 ) ;
#8255=CARTESIAN_POINT ( 'NONE',  ( -2.000000000000000000, -7.851777359433979697, -3.255701506262516087 ) ) ;
#8256=ORIENTED_EDGE ( 'NONE', *, *, #4869, .T. ) ;
#8260=DIRECTION ( 'NONE',  ( -1.000000000000000000, 0.000000000000000000, -0.000000000000000000 ) ) ;
#8263=ORIENTED_EDGE ( 'NONE', *, *, #10127, .F. ) ;
#8266=VERTEX_POINT ( 'NONE', #4685 ) ;
#8275=DIRECTION ( 'NONE',  ( -1.000000000000000000, -0.000000000000000000, 0.000000000000000000 ) ) ;
#8282=ORIENTED_EDGE ( 'NONE', *, *, #6981, .T. ) ;
#8288=FACE_OUTER_BOUND ( 'NONE', #9265, .T. ) ;
#8291=CYLINDRICAL_SURFACE ( 'NONE', #5984, 3.000000000000000000 ) ;
#8296=CARTESIAN_POINT ( 'NONE',  ( -2.000000000000000000, -6.700937042937042065, -2.183447440113260196 ) ) ;
#8298=CIRCLE ( 'NONE', #3206, 6.248999999999999666 ) ;
#8303=CIRCLE ( 'NONE', #337, 3.000000000000000000 ) ;
#8314=ORIENTED_EDGE ( 'NONE', *, *, #8066, .F. ) ;
#8316=CIRCLE ( 'NONE', #9675, 3.000000000000000000 ) ;
#8318=ORIENTED_EDGE ( 'NONE', *, *, #3635, .T. ) ;
#8321=ADVANCED_FACE ( 'NONE', ( #4256 ), #5108, .T. ) ;
#8323=AXIS2_PLACEMENT_3D ( 'NONE', #10117, #1199, #2051 ) ;
#8330=CIRCLE ( 'NONE', #5096, 3.000000000000000000 ) ;
#8331=CARTESIAN_POINT ( 'NONE',  ( 8.000000000000001776, -7.009698679648282749, -0.7308381473897593850 ) ) ;
#8335=DIRECTION ( 'NONE',  ( -1.000000000000000000, -0.000000000000000000, -0.000000000000000000 ) ) ;
#8347=SHAPE_REPRESENTATION ( 'jaw_ISO - Spur gear 1M 15T 20PA 8FW ---S15A75H50L4.0N', ( #2101 ), #5648 ) ;
#8353=DIRECTION ( 'NONE',  ( -1.000000000000000000, 0.000000000000000000, -0.000000000000000000 ) ) ;
#8357=CIRCLE ( 'NONE', #3439, 3.000000000000000000 ) ;
#8363=ADVANCED_FACE ( 'NONE', ( #5889 ), #8932, .T. ) ;
#8365=AXIS2_PLACEMENT_3D ( 'NONE', #2669, #1025, #2570 ) ;
#8366=LINE ( 'NONE', #10164, #3489 ) ;
#8376=EDGE_LOOP ( 'NONE', ( #8672, #7314, #3291, #4589 ) ) ;
#8377=CARTESIAN_POINT ( 'NONE',  ( 8.000000000000001776, -6.106419733534973915, -3.518755179752866447 ) ) ;
#8381=FACE_OUTER_BOUND ( 'NONE', #8789, .T. ) ;
#8386=CARTESIAN_POINT ( 'NONE',  ( 10.00000000000000000, -7.673322273190701814, -3.656518192455153748 ) ) ;
#8393=LINE ( 'NONE', #10043, #2481 ) ;
#8403=VERTEX_POINT ( 'NONE', #7345 ) ;
#8409=CIRCLE ( 'NONE', #2985, 3.000000000000000000 ) ;
#8416=ORIENTED_EDGE ( 'NONE', *, *, #9000, .T. ) ;
#8417=ADVANCED_FACE ( 'NONE', ( #7289 ), #2626, .F. ) ;
#8424=VERTEX_POINT ( 'NONE', #4053 ) ;
#8427=( NAMED_UNIT ( * ) SI_UNIT ( $, .STERADIAN. ) SOLID_ANGLE_UNIT ( ) );
#8442=LINE ( 'NONE', #6033, #7038 ) ;
#8445=ADVANCED_FACE ( 'NONE', ( #6487 ), #3314, .T. ) ;
#8446=EDGE_CURVE ( 'NONE', #4422, #5902, #190, .T. ) ;
#8459=AXIS2_PLACEMENT_3D ( 'NONE', #7084, #4761, #3913 ) ;
#8464=ORIENTED_EDGE ( 'NONE', *, *, #5687, .T. ) ;
#8475=ADVANCED_FACE ( 'NONE', ( #1780 ), #8253, .T. ) ;
#8482=FACE_OUTER_BOUND ( 'NONE', #5447, .T. ) ;
#8485=DIRECTION ( 'NONE',  ( 0.000000000000000000, 0.000000000000000000, 1.000000000000000000 ) ) ;
#8491=CARTESIAN_POINT ( 'NONE',  ( 4.000000000000000888, -8.497168642645963388, -0.2193742428685764301 ) ) ;
#8513=VERTEX_POINT ( 'NONE', #2880 ) ;
#8519=AXIS2_PLACEMENT_3D ( 'NONE', #7894, #2225, #2854 ) ;
#8539=CARTESIAN_POINT ( 'NONE',  ( -2.000000000000000000, -7.851777359434023218, 3.255701506262409506 ) ) ;
#8541=VECTOR ( 'NONE', #2379, 1000.000000000000000 ) ;
#8550=EDGE_CURVE ( 'NONE', #3855, #10281, #1883, .T. ) ;
#8556=FACE_OUTER_BOUND ( 'NONE', #9363, .T. ) ;
#8566=ORIENTED_EDGE ( 'NONE', *, *, #7438, .T. ) ;
#8567=AXIS2_PLACEMENT_3D ( 'NONE', #2923, #6889, #435 ) ;
#8572=ORIENTED_EDGE ( 'NONE', *, *, #4408, .F. ) ;
#8577=ADVANCED_FACE ( 'NONE', ( #6106 ), #9356, .T. ) ;
#8580=VERTEX_POINT ( 'NONE', #6797 ) ;
#8581=CARTESIAN_POINT ( 'NONE',  ( -2.000000000000000000, -4.724769925181144359, -4.089810527897808079 ) ) ;
#8585=DIRECTION ( 'NONE',  ( -1.000000000000000000, -0.000000000000000000, -0.000000000000000000 ) ) ;
#8587=EDGE_LOOP ( 'NONE', ( #9573, #6498, #3744, #10386 ) ) ;
#8589=DIRECTION ( 'NONE',  ( -1.000000000000000000, -0.000000000000000000, -0.000000000000000000 ) ) ;
#8613=EDGE_CURVE ( 'NONE', #8266, #8842, #2727, .T. ) ;
#8617=CIRCLE ( 'NONE', #7774, 3.000000000000000000 ) ;
#8620=CIRCLE ( 'NONE', #2535, 6.248999999999999666 ) ;
#8627=AXIS2_PLACEMENT_3D ( 'NONE', #7881, #3211, #3318 ) ;
#8630=ORIENTED_EDGE ( 'NONE', *, *, #4777, .T. ) ;
#8631=CARTESIAN_POINT ( 'NONE',  ( 8.000000000000001776, 0.000000000000000000, 0.000000000000000000 ) ) ;
#8634=ORIENTED_EDGE ( 'NONE', *, *, #4359, .F. ) ;
#8637=VECTOR ( 'NONE', #6243, 1000.000000000000000 ) ;
#8638=DIRECTION ( 'NONE',  ( 0.000000000000000000, 0.000000000000000000, -1.000000000000000000 ) ) ;
#8643=DIRECTION ( 'NONE',  ( 0.000000000000000000, 1.807003620809173399E-15, -1.000000000000000000 ) ) ;
#8645=AXIS2_PLACEMENT_3D ( 'NONE', #4512, #10255, #2988 ) ;
#8648=CARTESIAN_POINT ( 'NONE',  ( 8.000000000000001776, -5.979767908488852868, 1.814490771706165351 ) ) ;
#8657=DIRECTION ( 'NONE',  ( 0.000000000000000000, 0.000000000000000000, -1.000000000000000000 ) ) ;
#8661=DIRECTION ( 'NONE',  ( -1.000000000000000000, 0.000000000000000000, 0.000000000000000000 ) ) ;
#8672=ORIENTED_EDGE ( 'NONE', *, *, #6734, .F. ) ;
#8680=ORIENTED_EDGE ( 'NONE', *, *, #2477, .T. ) ;
#8683=VERTEX_POINT ( 'NONE', #6208 ) ;
#8691=LINE ( 'NONE', #10290, #2764 ) ;
#8692=DIRECTION ( 'NONE',  ( 0.000000000000000000, 0.000000000000000000, -1.000000000000000000 ) ) ;
#8695=CYLINDRICAL_SURFACE ( 'NONE', #8567, 2.000000000000000000 ) ;
#8697=DIRECTION ( 'NONE',  ( 0.000000000000000000, 0.000000000000000000, -1.000000000000000000 ) ) ;
#8712=VECTOR ( 'NONE', #6524, 1000.000000000000000 ) ;
#8716=ORIENTED_EDGE ( 'NONE', *, *, #1637, .F. ) ;
#8717=VERTEX_POINT ( 'NONE', #3040 ) ;
#8726=EDGE_CURVE ( 'NONE', #935, #4422, #8822, .T. ) ;
#8747=DIRECTION ( 'NONE',  ( 0.000000000000000000, 1.000000000000000000, -7.228014483236698281E-18 ) ) ;
#8756=ORIENTED_EDGE ( 'NONE', *, *, #6140, .T. ) ;
#8760=EDGE_CURVE ( 'NONE', #10319, #9335, #710, .T. ) ;
#8761=ORIENTED_EDGE ( 'NONE', *, *, #8550, .T. ) ;
#8765=PRODUCT_DEFINITION_SHAPE ( 'NONE', 'NONE',  #8792 ) ;
#8766=VERTEX_POINT ( 'NONE', #10423 ) ;
#8771=ORIENTED_EDGE ( 'NONE', *, *, #10472, .T. ) ;
#8776=EDGE_LOOP ( 'NONE', ( #5692, #133, #1053, #1049 ) ) ;
#8778=DIRECTION ( 'NONE',  ( -1.000000000000000000, -0.000000000000000000, 0.000000000000000000 ) ) ;
#8780=ORIENTED_EDGE ( 'NONE', *, *, #2801, .T. ) ;
#8781=CARTESIAN_POINT ( 'NONE',  ( 10.00000000000000000, 52.93638525830372998, 8.843061888689529582 ) ) ;
#8789=EDGE_LOOP ( 'NONE', ( #6963, #5734, #10371, #720 ) ) ;
#8790=CARTESIAN_POINT ( 'NONE',  ( 10.00000000000000000, -7.673322273190750664, 3.656518192455050276 ) ) ;
#8792=PRODUCT_DEFINITION ( 'UNKNOWN', '', #2290, #10487 ) ;
#8805=AXIS2_PLACEMENT_3D ( 'NONE', #1531, #1473, #9542 ) ;
#8808=CIRCLE ( 'NONE', #4392, 6.248999999999999666 ) ;
#8820=ORIENTED_EDGE ( 'NONE', *, *, #227, .F. ) ;
#8822=LINE ( 'NONE', #9520, #7298 ) ;
#8827=ADVANCED_FACE ( 'NONE', ( #6312 ), #3145, .T. ) ;
#8832=ORIENTED_EDGE ( 'NONE', *, *, #1348, .T. ) ;
#8842=VERTEX_POINT ( 'NONE', #2565 ) ;
#8843=ORIENTED_EDGE ( 'NONE', *, *, #610, .T. ) ;
#8847=EDGE_LOOP ( 'NONE', ( #6079, #7363, #9105, #6606 ) ) ;
#8851=ORIENTED_EDGE ( 'NONE', *, *, #2477, .F. ) ;
#8856=CARTESIAN_POINT ( 'NONE',  ( 10.00000000000000000, -6.700937042937042065, -2.183447440113260196 ) ) ;
#8860=DIRECTION ( 'NONE',  ( -1.000000000000000000, 0.000000000000000000, 0.000000000000000000 ) ) ;
#8869=EDGE_CURVE ( 'NONE', #3855, #8167, #24, .T. ) ;
#8883=DIRECTION ( 'NONE',  ( -1.000000000000000000, 0.000000000000000000, 0.000000000000000000 ) ) ;
#8888=DIRECTION ( 'NONE',  ( -1.000000000000000000, -0.000000000000000000, 0.000000000000000000 ) ) ;
#8897=ADVANCED_FACE ( 'NONE', ( #8381 ), #6824, .T. ) ;
#8900=CARTESIAN_POINT ( 'NONE',  ( 10.00000000000000000, 0.000000000000000000, 0.000000000000000000 ) ) ;
#8919=CARTESIAN_POINT ( 'NONE',  ( -2.000000000000000000, 0.000000000000000000, 0.000000000000000000 ) ) ;
#8922=CYLINDRICAL_SURFACE ( 'NONE', #1801, 3.000000000000000000 ) ;
#8932=CYLINDRICAL_SURFACE ( 'NONE', #27, 8.500000000000000000 ) ;
#8934=DIRECTION ( 'NONE',  ( -1.000000000000000000, -0.000000000000000000, -0.000000000000000000 ) ) ;
#8935=LINE ( 'NONE', #196, #2875 ) ;
#8939=VERTEX_POINT ( 'NONE', #7383 ) ;
#8988=AXIS2_PLACEMENT_3D ( 'NONE', #5942, #5269, #1239 ) ;
#8998=ORIENTED_EDGE ( 'NONE', *, *, #4549, .F. ) ;
#9000=EDGE_CURVE ( 'NONE', #8167, #4491, #2275, .T. ) ;
#9001=FACE_OUTER_BOUND ( 'NONE', #1100, .T. ) ;
#9010=( NAMED_UNIT ( * ) PLANE_ANGLE_UNIT ( ) SI_UNIT ( $, .RADIAN. ) );
#9011=ORIENTED_EDGE ( 'NONE', *, *, #6094, .F. ) ;
#9015=ORIENTED_EDGE ( 'NONE', *, *, #6863, .T. ) ;
#9028=CARTESIAN_POINT ( 'NONE',  ( 8.000000000000001776, -4.147285340411748678, -5.698247474649444477 ) ) ;
#9037=DIRECTION ( 'NONE',  ( 1.000000000000000000, 0.000000000000000000, 0.000000000000000000 ) ) ;
#9050=VERTEX_POINT ( 'NONE', #6186 ) ;
#9053=ORIENTED_EDGE ( 'NONE', *, *, #2403, .F. ) ;
#9069=EDGE_CURVE ( 'NONE', #7252, #8266, #10392, .T. ) ;
#9085=CARTESIAN_POINT ( 'NONE',  ( 0.000000000000000000, -7.063614741696270016, 8.843061888689529582 ) ) ;
#9091=EDGE_CURVE ( 'NONE', #837, #9494, #8357, .T. ) ;
#9095=DIRECTION ( 'NONE',  ( 0.000000000000000000, -0.000000000000000000, -1.000000000000000000 ) ) ;
#9096=VERTEX_POINT ( 'NONE', #2068 ) ;
#9105=ORIENTED_EDGE ( 'NONE', *, *, #5772, .T. ) ;
#9119=CARTESIAN_POINT ( 'NONE',  ( 50.00005079999999680, 0.000000000000000000, 0.000000000000000000 ) ) ;
#9125=DIRECTION ( 'NONE',  ( -1.000000000000000000, -0.000000000000000000, -0.000000000000000000 ) ) ;
#9127=DIRECTION ( 'NONE',  ( -1.000000000000000000, 0.000000000000000000, 0.000000000000000000 ) ) ;
#9128=AXIS2_PLACEMENT_3D ( 'NONE', #5561, #1602, #803 ) ;
#9133=CIRCLE ( 'NONE', #7269, 3.000000000000000000 ) ;
#9159=ORIENTED_EDGE ( 'NONE', *, *, #9234, .T. ) ;
#9167=AXIS2_PLACEMENT_3D ( 'NONE', #7500, #6590, #9743 ) ;
#9170=ORIENTED_EDGE ( 'NONE', *, *, #4047, .F. ) ;
#9171=VECTOR ( 'NONE', #8353, 1000.000000000000000 ) ;
#9184=CARTESIAN_POINT ( 'NONE',  ( 8.000000000000001776, 0.000000000000000000, 0.000000000000000000 ) ) ;
#9186=CARTESIAN_POINT ( 'NONE',  ( 10.00000000000000000, -6.106419733534973915, -3.518755179752866447 ) ) ;
#9192=VERTEX_POINT ( 'NONE', #4071 ) ;
#9196=DIRECTION ( 'NONE',  ( 0.000000000000000000, 0.000000000000000000, 1.000000000000000000 ) ) ;
#9215=STYLED_ITEM ( 'NONE', ( #1055 ), #689 ) ;
#9216=ORIENTED_EDGE ( 'NONE', *, *, #5479, .F. ) ;
#9218=CARTESIAN_POINT ( 'NONE',  ( 10.00000000000000000, -6.700937042937071375, 2.183447440113169602 ) ) ;
#9219=EDGE_CURVE ( 'NONE', #8766, #5625, #1234, .T. ) ;
#9234=EDGE_CURVE ( 'NONE', #467, #8766, #10340, .T. ) ;
#9238=LINE ( 'NONE', #1977, #3491 ) ;
#9239=CARTESIAN_POINT ( 'NONE',  ( -2.000000000000000000, -7.063614741696270016, 8.843061888689529582 ) ) ;
#9245=VECTOR ( 'NONE', #4619, 1000.000000000000000 ) ;
#9246=ORIENTED_EDGE ( 'NONE', *, *, #2027, .T. ) ;
#9249=AXIS2_PLACEMENT_3D ( 'NONE', #8856, #5711, #3287 ) ;
#9250=DIRECTION ( 'NONE',  ( -1.000000000000000000, -0.000000000000000000, -0.000000000000000000 ) ) ;
#9256=ORIENTED_EDGE ( 'NONE', *, *, #5376, .F. ) ;
#9257=ORIENTED_EDGE ( 'NONE', *, *, #9802, .F. ) ;
#9261=ORIENTED_EDGE ( 'NONE', *, *, #1997, .T. ) ;
#9265=EDGE_LOOP ( 'NONE', ( #240, #5312, #101, #9813 ) ) ;
#9266=CARTESIAN_POINT ( 'NONE',  ( 8.000000000000001776, -6.700937042937071375, 2.183447440113169602 ) ) ;
#9267=UNCERTAINTY_MEASURE_WITH_UNIT (LENGTH_MEASURE( 1.000000000000000082E-05 ), #5180, 'distance_accuracy_value', 'NONE');
#9277=EDGE_LOOP ( 'NONE', ( #4135, #9532, #2517, #8314 ) ) ;
#9278=DIRECTION ( 'NONE',  ( -1.000000000000000000, -0.000000000000000000, -0.000000000000000000 ) ) ;
#9279=EDGE_CURVE ( 'NONE', #1830, #4156, #9390, .T. ) ;
#9282=CARTESIAN_POINT ( 'NONE',  ( 10.00000000000000000, -7.063614741696270016, 3.730353617970412206 ) ) ;
#9297=DIRECTION ( 'NONE',  ( -1.000000000000000000, -0.000000000000000000, -0.000000000000000000 ) ) ;
#9299=EDGE_LOOP ( 'NONE', ( #10002, #8843, #9606, #890 ) ) ;
#9305=ORIENTED_EDGE ( 'NONE', *, *, #1613, .T. ) ;
#9315=EDGE_CURVE ( 'NONE', #9096, #7164, #8042, .T. ) ;
#9322=AXIS2_PLACEMENT_3D ( 'NONE', #6210, #5473, #652 ) ;
#9329=DIRECTION ( 'NONE',  ( 0.000000000000000000, 0.000000000000000000, -1.000000000000000000 ) ) ;
#9335=VERTEX_POINT ( 'NONE', #2436 ) ;
#9337=CIRCLE ( 'NONE', #185, 3.000000000000000000 ) ;
#9339=CIRCLE ( 'NONE', #34, 3.000000000000000000 ) ;
#9343=EDGE_CURVE ( 'NONE', #8683, #145, #3462, .T. ) ;
#9356=PLANE ( 'NONE',  #693 ) ;
#9363=EDGE_LOOP ( 'NONE', ( #5063, #8761, #3155, #9482 ) ) ;
#9364=ORIENTED_EDGE ( 'NONE', *, *, #2265, .F. ) ;
#9366=CYLINDRICAL_SURFACE ( 'NONE', #4750, 6.248999999999999666 ) ;
#9368=LINE ( 'NONE', #559, #6087 ) ;
#9369=ORIENTED_EDGE ( 'NONE', *, *, #10472, .F. ) ;
#9373=ORIENTED_EDGE ( 'NONE', *, *, #2027, .F. ) ;
#9381=ORIENTED_EDGE ( 'NONE', *, *, #2733, .T. ) ;
#9383=CARTESIAN_POINT ( 'NONE',  ( 10.00000000000000000, 7.008469740302802897, 0.7425307242148025955 ) ) ;
#9386=CARTESIAN_POINT ( 'NONE',  ( 8.000000000000001776, -6.200809695932771426, -0.7745709230445765314 ) ) ;
#9388=DIRECTION ( 'NONE',  ( 0.000000000000000000, 2.309263891220325920E-14, -1.000000000000000000 ) ) ;
#9390=CIRCLE ( 'NONE', #8208, 8.500000000000000000 ) ;
#9392=DIRECTION ( 'NONE',  ( -1.000000000000000000, -0.000000000000000000, -0.000000000000000000 ) ) ;
#9395=CARTESIAN_POINT ( 'NONE',  ( -2.000000000000000000, 0.000000000000000000, 0.000000000000000000 ) ) ;
#9409=DIRECTION ( 'NONE',  ( 0.000000000000000000, 1.000000000000000000, -7.228014483236698281E-18 ) ) ;
#9410=ORIENTED_EDGE ( 'NONE', *, *, #2792, .T. ) ;
#9424=FACE_OUTER_BOUND ( 'NONE', #5022, .T. ) ;
#9425=DIRECTION ( 'NONE',  ( -1.000000000000000000, -0.000000000000000000, -0.000000000000000000 ) ) ;
#9426=EDGE_LOOP ( 'NONE', ( #2904, #3474, #8771, #3994 ) ) ;
#9429=ORIENTED_EDGE ( 'NONE', *, *, #3917, .F. ) ;
#9433=ORIENTED_EDGE ( 'NONE', *, *, #427, .T. ) ;
#9442=VERTEX_POINT ( 'NONE', #8539 ) ;
#9458=CARTESIAN_POINT ( 'NONE',  ( 10.00000000000000000, 8.357095590591340439, -1.552080310331536372 ) ) ;
#9468=CIRCLE ( 'NONE', #4371, 8.500000000000000000 ) ;
#9470=ORIENTED_EDGE ( 'NONE', *, *, #7065, .F. ) ;
#9474=ADVANCED_FACE ( 'NONE', ( #7744 ), #4445, .T. ) ;
#9476=EDGE_CURVE ( 'NONE', #7456, #6865, #7696, .T. ) ;
#9477=( GEOMETRIC_REPRESENTATION_CONTEXT ( 3 ) GLOBAL_UNCERTAINTY_ASSIGNED_CONTEXT ( ( #2061 ) ) GLOBAL_UNIT_ASSIGNED_CONTEXT ( ( #1397, #5528, #3094 ) ) REPRESENTATION_CONTEXT ( 'NONE', 'WORKASPACE' ) );
#9478=DIRECTION ( 'NONE',  ( 0.000000000000000000, 0.000000000000000000, 1.000000000000000000 ) ) ;
#9481=VECTOR ( 'NONE', #2616, 1000.000000000000000 ) ;
#9482=ORIENTED_EDGE ( 'NONE', *, *, #9000, .F. ) ;
#9487=CIRCLE ( 'NONE', #8627, 3.000000000000000000 ) ;
#9494=VERTEX_POINT ( 'NONE', #7793 ) ;
#9502=DIRECTION ( 'NONE',  ( 0.000000000000000000, 0.000000000000000000, 1.000000000000000000 ) ) ;
#9503=DIRECTION ( 'NONE',  ( 0.000000000000000000, 0.000000000000000000, 1.000000000000000000 ) ) ;
#9507=DIRECTION ( 'NONE',  ( 1.000000000000000000, 0.000000000000000000, 0.000000000000000000 ) ) ;
#9513=ORIENTED_EDGE ( 'NONE', *, *, #10459, .F. ) ;
#9520=CARTESIAN_POINT ( 'NONE',  ( 4.000000000000000888, -7.851777359433979697, -3.255701506262516087 ) ) ;
#9532=ORIENTED_EDGE ( 'NONE', *, *, #598, .T. ) ;
#9537=DIRECTION ( 'NONE',  ( 0.000000000000000000, 0.000000000000000000, 1.000000000000000000 ) ) ;
#9542=DIRECTION ( 'NONE',  ( 0.000000000000000000, 0.000000000000000000, 1.000000000000000000 ) ) ;
#9547=ORIENTED_EDGE ( 'NONE', *, *, #2530, .F. ) ;
#9554=EDGE_CURVE ( 'NONE', #8006, #5123, #8691, .T. ) ;
#9568=DIRECTION ( 'NONE',  ( 1.000000000000000000, -0.000000000000000000, -0.000000000000000000 ) ) ;
#9573=ORIENTED_EDGE ( 'NONE', *, *, #9829, .T. ) ;
#9581=ORIENTED_EDGE ( 'NONE', *, *, #1709, .T. ) ;
#9582=DIRECTION ( 'NONE',  ( 0.000000000000000000, 3.819167204710539130E-14, -1.000000000000000000 ) ) ;
#9589=LINE ( 'NONE', #7996, #8160 ) ;
#9597=ORIENTED_EDGE ( 'NONE', *, *, #213, .F. ) ;
#9598=CARTESIAN_POINT ( 'NONE',  ( -2.000000000000000000, -8.497168642645963388, -0.2193742428685764301 ) ) ;
#9605=CARTESIAN_POINT ( 'NONE',  ( -2.000000000000000000, 0.000000000000000000, 0.000000000000000000 ) ) ;
#9606=ORIENTED_EDGE ( 'NONE', *, *, #5429, .T. ) ;
#9609=CARTESIAN_POINT ( 'NONE',  ( -2.000000000000000000, 2.429606751577122026, -5.757344182232885466 ) ) ;
#9610=DIRECTION ( 'NONE',  ( -1.000000000000000000, 0.000000000000000000, -0.000000000000000000 ) ) ;
#9615=ADVANCED_FACE ( 'NONE', ( #1426 ), #7900, .T. ) ;
#9626=DIRECTION ( 'NONE',  ( -1.000000000000000000, 0.000000000000000000, -0.000000000000000000 ) ) ;
#9633=ADVANCED_FACE ( 'NONE', ( #5395, #4546 ), #4960, .F. ) ;
#9637=DIRECTION ( 'NONE',  ( 0.000000000000000000, 0.000000000000000000, -1.000000000000000000 ) ) ;
#9668=ORIENTED_EDGE ( 'NONE', *, *, #2748, .T. ) ;
#9675=AXIS2_PLACEMENT_3D ( 'NONE', #7001, #2933, #8657 ) ;
#9679=DIRECTION ( 'NONE',  ( 0.000000000000000000, 0.000000000000000000, -1.000000000000000000 ) ) ;
#9683=CIRCLE ( 'NONE', #188, 6.248999999999999666 ) ;
#9689=CIRCLE ( 'NONE', #6446, 6.248999999999999666 ) ;
#9691=VERTEX_POINT ( 'NONE', #7558 ) ;
#9695=ORIENTED_EDGE ( 'NONE', *, *, #8726, .F. ) ;
#9696=CARTESIAN_POINT ( 'NONE',  ( 8.000000000000001776, 6.226349476952025341, -0.5315761383463619705 ) ) ;
#9715=CARTESIAN_POINT ( 'NONE',  ( 8.000000000000001776, 6.226349476952025341, 0.5315761383463611933 ) ) ;
#9717=DIRECTION ( 'NONE',  ( 1.000000000000000000, 0.000000000000000000, -0.000000000000000000 ) ) ;
#9718=CARTESIAN_POINT ( 'NONE',  ( 10.00000000000000000, -5.979767908488852868, 1.814490771706165351 ) ) ;
#9743=DIRECTION ( 'NONE',  ( 0.000000000000000000, 0.000000000000000000, 1.000000000000000000 ) ) ;
#9771=VECTOR ( 'NONE', #9610, 1000.000000000000000 ) ;
#9774=EDGE_LOOP ( 'NONE', ( #9364, #10156, #7295, #9159 ) ) ;
#9777=DIRECTION ( 'NONE',  ( 0.000000000000000000, 0.000000000000000000, 1.000000000000000000 ) ) ;
#9784=CARTESIAN_POINT ( 'NONE',  ( 10.00000000000000000, 0.000000000000000000, 0.000000000000000000 ) ) ;
#9791=EDGE_CURVE ( 'NONE', #1449, #4422, #4615, .T. ) ;
#9799=CARTESIAN_POINT ( 'NONE',  ( 10.00000000000000000, 0.000000000000000000, 0.000000000000000000 ) ) ;
#9802=EDGE_CURVE ( 'NONE', #1645, #2644, #5465, .T. ) ;
#9813=ORIENTED_EDGE ( 'NONE', *, *, #2708, .T. ) ;
#9827=AXIS2_PLACEMENT_3D ( 'NONE', #9836, #1614, #5780 ) ;
#9829=EDGE_CURVE ( 'NONE', #2344, #7761, #61, .T. ) ;
#9832=DIRECTION ( 'NONE',  ( 0.000000000000000000, 0.000000000000000000, -1.000000000000000000 ) ) ;
#9834=CARTESIAN_POINT ( 'NONE',  ( 10.00000000000000000, 6.100541242131515496, 3.528937025535514138 ) ) ;
#9836=CARTESIAN_POINT ( 'NONE',  ( 8.000000000000001776, -6.700937042937042065, -2.183447440113260196 ) ) ;
#9841=AXIS2_PLACEMENT_3D ( 'NONE', #4891, #6424, #10484 ) ;
#9848=DIRECTION ( 'NONE',  ( 0.000000000000000000, 0.000000000000000000, 1.000000000000000000 ) ) ;
#9853=CARTESIAN_POINT ( 'NONE',  ( -2.000000000000000000, 0.000000000000000000, 0.000000000000000000 ) ) ;
#9854=ORIENTED_EDGE ( 'NONE', *, *, #6108, .F. ) ;
#9886=DIRECTION ( 'NONE',  ( 1.000000000000000000, 0.000000000000000000, 0.000000000000000000 ) ) ;
#9908=ORIENTED_EDGE ( 'NONE', *, *, #4152, .T. ) ;
#9936=AXIS2_PLACEMENT_3D ( 'NONE', #6739, #2776, #5991 ) ;
#9941=DIRECTION ( 'NONE',  ( -1.000000000000000000, -0.000000000000000000, -0.000000000000000000 ) ) ;
#9948=ADVANCED_FACE ( 'NONE', ( #5409 ), #2343, .T. ) ;
#9958=EDGE_LOOP ( 'NONE', ( #5077, #3416, #7600, #1558 ) ) ;
#9961=ADVANCED_FACE ( 'NONE', ( #6305 ), #3191, .T. ) ;
#9974=VERTEX_POINT ( 'NONE', #2402 ) ;
#9996=VERTEX_POINT ( 'NONE', #591 ) ;
#10001=CARTESIAN_POINT ( 'NONE',  ( 0.000000000000000000, -7.063614741696270016, 2.343061888689530026 ) ) ;
#10002=ORIENTED_EDGE ( 'NONE', *, *, #2326, .T. ) ;
#10016=CIRCLE ( 'NONE', #5424, 8.500000000000000000 ) ;
#10026=VECTOR ( 'NONE', #7075, 1000.000000000000000 ) ;
#10030=CARTESIAN_POINT ( 'NONE',  ( 4.000000000000000888, 8.265874651078018331, 1.981241088980807419 ) ) ;
#10041=DIRECTION ( 'NONE',  ( 1.000000000000000000, 0.000000000000000000, -0.000000000000000000 ) ) ;
#10043=CARTESIAN_POINT ( 'NONE',  ( 8.000000000000001776, 2.429606751577122026, -5.757344182232885466 ) ) ;
#10050=ORIENTED_EDGE ( 'NONE', *, *, #3777, .F. ) ;
#10054=ORIENTED_EDGE ( 'NONE', *, *, #2913, .T. ) ;
#10064=DIRECTION ( 'NONE',  ( -1.000000000000000000, 0.000000000000000000, 0.000000000000000000 ) ) ;
#10068=EDGE_CURVE ( 'NONE', #9442, #9691, #7160, .T. ) ;
#10073=AXIS2_PLACEMENT_3D ( 'NONE', #1482, #4654, #6988 ) ;
#10078=ORIENTED_EDGE ( 'NONE', *, *, #3622, .T. ) ;
#10080=CYLINDRICAL_SURFACE ( 'NONE', #1010, 3.000000000000000000 ) ;
#10082=CARTESIAN_POINT ( 'NONE',  ( 10.00000000000000000, -8.497168642645966941, 0.2193742428684610779 ) ) ;
#10094=LINE ( 'NONE', #1924, #9481 ) ;
#10097=AXIS2_PLACEMENT_3D ( 'NONE', #9184, #3558, #6785 ) ;
#10106=CIRCLE ( 'NONE', #5518, 2.000000000000000000 ) ;
#10112=EDGE_LOOP ( 'NONE', ( #8820, #1463, #9015, #6971, #3526, #3680, #8256, #2774, #9305, #1907, #5715, #7087, #2848, #6714, #1353, #6073, #8416, #7458, #739, #2881, #6320, #4865, #9908, #1401, #9410, #4518, #6844, #5748, #4088, #5804, #6542, #1214, #6313, #563, #1457, #9668, #35, #9257, #2201, #7078, #8566, #962, #7865, #10078, #413, #2008 ) ) ;
#10117=CARTESIAN_POINT ( 'NONE',  ( 10.00000000000000000, 2.871924938129970517, -6.435996203144478400 ) ) ;
#10127=EDGE_CURVE ( 'NONE', #8717, #4944, #70, .T. ) ;
#10129=DIRECTION ( 'NONE',  ( 0.000000000000000000, 0.000000000000000000, 1.000000000000000000 ) ) ;
#10132=DIRECTION ( 'NONE',  ( -1.000000000000000000, 0.000000000000000000, 0.000000000000000000 ) ) ;
#10140=CARTESIAN_POINT ( 'NONE',  ( -2.000000000000000000, 0.000000000000000000, 0.000000000000000000 ) ) ;
#10154=DIRECTION ( 'NONE',  ( 0.000000000000000000, 0.000000000000000000, 1.000000000000000000 ) ) ;
#10156=ORIENTED_EDGE ( 'NONE', *, *, #3828, .F. ) ;
#10164=CARTESIAN_POINT ( 'NONE',  ( 8.000000000000001776, 5.793104693147763662, 2.343061888689530026 ) ) ;
#10165=DIRECTION ( 'NONE',  ( -1.000000000000000000, 0.000000000000000000, 0.000000000000000000 ) ) ;
#10171=DIRECTION ( 'NONE',  ( 0.000000000000000000, 1.000000000000000000, -7.228014483236699822E-18 ) ) ;
#10174=EDGE_CURVE ( 'NONE', #10267, #2046, #1414, .T. ) ;
#10177=AXIS2_PLACEMENT_3D ( 'NONE', #3617, #7707, #6845 ) ;
#10183=ORIENTED_EDGE ( 'NONE', *, *, #6350, .T. ) ;
#10184=DIRECTION ( 'NONE',  ( 0.000000000000000000, 0.000000000000000000, 1.000000000000000000 ) ) ;
#10198=CARTESIAN_POINT ( 'NONE',  ( 10.00000000000000000, 1.418488851014483076, -6.085876303339363247 ) ) ;
#10218=CARTESIAN_POINT ( 'NONE',  ( 8.000000000000001776, 0.000000000000000000, 0.000000000000000000 ) ) ;
#10228=AXIS2_PLACEMENT_3D ( 'NONE', #9799, #8260, #1788 ) ;
#10229=ORIENTED_EDGE ( 'NONE', *, *, #1247, .T. ) ;
#10234=CARTESIAN_POINT ( 'NONE',  ( 10.00000000000000000, -7.063614741696270016, 8.843061888689529582 ) ) ;
#10253=VERTEX_POINT ( 'NONE', #4343 ) ;
#10255=DIRECTION ( 'NONE',  ( -1.000000000000000000, -0.000000000000000000, -0.000000000000000000 ) ) ;
#10263=CARTESIAN_POINT ( 'NONE',  ( -2.000000000000000000, 4.561279057474473930, -4.271385531633122845 ) ) ;
#10267=VERTEX_POINT ( 'NONE', #5141 ) ;
#10274=ORIENTED_EDGE ( 'NONE', *, *, #2792, .F. ) ;
#10277=EDGE_LOOP ( 'NONE', ( #10054, #296, #683, #4354 ) ) ;
#10279=EDGE_LOOP ( 'NONE', ( #4119, #10390, #1080, #4062 ) ) ;
#10281=VERTEX_POINT ( 'NONE', #1321 ) ;
#10288=ORIENTED_EDGE ( 'NONE', *, *, #5583, .T. ) ;
#10290=CARTESIAN_POINT ( 'NONE',  ( 4.000000000000000888, -2.417132211460011337, -8.149077976821821778 ) ) ;
#10292=PRODUCT ( 'jaw_ISO - Spur gear 1M 15T 20PA 8FW ---S15A75H50L4.0N', 'jaw_ISO - Spur gear 1M 15T 20PA 8FW ---S15A75H50L4.0N', '', ( #2456 ) ) ;
#10295=DIRECTION ( 'NONE',  ( -1.000000000000000000, 0.000000000000000000, 0.000000000000000000 ) ) ;
#10319=VERTEX_POINT ( 'NONE', #9282 ) ;
#10324=ORIENTED_EDGE ( 'NONE', *, *, #6732, .F. ) ;
#10331=ORIENTED_EDGE ( 'NONE', *, *, #610, .F. ) ;
#10336=AXIS2_PLACEMENT_3D ( 'NONE', #5892, #5847, #7602 ) ;
#10340=LINE ( 'NONE', #1641, #8541 ) ;
#10343=EDGE_CURVE ( 'NONE', #1958, #4156, #2815, .T. ) ;
#10346=AXIS2_PLACEMENT_3D ( 'NONE', #7230, #3305, #5529 ) ;
#10351=AXIS2_PLACEMENT_3D ( 'NONE', #6957, #9250, #1987 ) ;
#10352=CARTESIAN_POINT ( 'NONE',  ( 10.00000000000000000, 6.226349476952025341, -0.5315761383463619705 ) ) ;
#10354=DIRECTION ( 'NONE',  ( -1.000000000000000000, -0.000000000000000000, -0.000000000000000000 ) ) ;
#10355=APPLICATION_CONTEXT ( 'automotive_design' ) ;
#10357=FACE_OUTER_BOUND ( 'NONE', #141, .T. ) ;
#10362=EDGE_CURVE ( 'NONE', #8513, #4283, #6138, .T. ) ;
#10364=ORIENTED_EDGE ( 'NONE', *, *, #3976, .F. ) ;
#10366=DIRECTION ( 'NONE',  ( -1.000000000000000000, 0.000000000000000000, -0.000000000000000000 ) ) ;
#10367=DIRECTION ( 'NONE',  ( -1.000000000000000000, -0.000000000000000000, -0.000000000000000000 ) ) ;
#10371=ORIENTED_EDGE ( 'NONE', *, *, #7852, .T. ) ;
#10378=ORIENTED_EDGE ( 'NONE', *, *, #6981, .F. ) ;
#10379=CARTESIAN_POINT ( 'NONE',  ( -2.000000000000000000, -6.700937042937071375, 2.183447440113169602 ) ) ;
#10386=ORIENTED_EDGE ( 'NONE', *, *, #3658, .F. ) ;
#10390=ORIENTED_EDGE ( 'NONE', *, *, #8236, .F. ) ;
#10392=CIRCLE ( 'NONE', #8519, 6.248999999999999666 ) ;
#10393=EDGE_CURVE ( 'NONE', #5625, #5471, #4130, .T. ) ;
#10397=ORIENTED_EDGE ( 'NONE', *, *, #9829, .F. ) ;
#10401=EDGE_LOOP ( 'NONE', ( #9470, #4984, #5010, #10324 ) ) ;
#10423=CARTESIAN_POINT ( 'NONE',  ( -2.000000000000000000, 5.471841788314748989, -3.018103451449677621 ) ) ;
#10428=CIRCLE ( 'NONE', #7016, 2.000000000000000000 ) ;
#10441=CARTESIAN_POINT ( 'NONE',  ( 8.000000000000001776, -2.652816298622379776, -5.657964889053610946 ) ) ;
#10449=ORIENTED_EDGE ( 'NONE', *, *, #9234, .F. ) ;
#10454=DIRECTION ( 'NONE',  ( -1.000000000000000000, -0.000000000000000000, -0.000000000000000000 ) ) ;
#10459=EDGE_CURVE ( 'NONE', #4861, #5532, #6827, .T. ) ;
#10472=EDGE_CURVE ( 'NONE', #3105, #216, #913, .T. ) ;
#10473=ADVANCED_FACE ( 'NONE', ( #2231, #7950 ), #580, .F. ) ;
#10475=DIRECTION ( 'NONE',  ( -1.000000000000000000, 0.000000000000000000, 0.000000000000000000 ) ) ;
#10479=ORIENTED_EDGE ( 'NONE', *, *, #6734, .T. ) ;
#10484=DIRECTION ( 'NONE',  ( 0.000000000000000000, 0.000000000000000000, -1.000000000000000000 ) ) ;
#10487=PRODUCT_DEFINITION_CONTEXT ( 'detailed design', #2562, 'design' ) ;
#10494=DIRECTION ( 'NONE',  ( 0.000000000000000000, 0.000000000000000000, -1.000000000000000000 ) ) ;
ENDSEC;
END-ISO-10303-21;
